ISO-10303-21;
HEADER;
FILE_DESCRIPTION (('STEP AP214'),
    '1' );
FILE_NAME ('spur gear_iso_ISO - Spur gear 2M 18T 20PA 8FW ---S18A75H50L8.0S1.step',
    '2026-09-28T15:49:00',
    ( '' ),
    ( '' ),
    'SwSTEP 2.0',
    'SolidWorks 2026',
    '' );
FILE_SCHEMA (( 'AUTOMOTIVE_DESIGN' ));
ENDSEC;

DATA;
#1=CARTESIAN_POINT ( 'NONE',  ( 8.000000000000000000, -16.59870953437682672, 3.253005020243791456 ) ) ;
#7=DIRECTION ( 'NONE',  ( -1.000000000000000000, 0.000000000000000000, 0.000000000000000000 ) ) ;
#15=ORIENTED_EDGE ( 'NONE', *, *, #2696, .T. ) ;
#19=ORIENTED_EDGE ( 'NONE', *, *, #4802, .F. ) ;
#31=ADVANCED_FACE ( 'NONE', ( #16880 ), #5577, .T. ) ;
#43=DIRECTION ( 'NONE',  ( -1.000000000000000000, 0.000000000000000000, 0.000000000000000000 ) ) ;
#72=FACE_OUTER_BOUND ( 'NONE', #19048, .T. ) ;
#90=ORIENTED_EDGE ( 'NONE', *, *, #30599, .T. ) ;
#109=FACE_OUTER_BOUND ( 'NONE', #11807, .T. ) ;
#112=DIRECTION ( 'NONE',  ( -1.000000000000000000, 0.000000000000000000, 0.000000000000000000 ) ) ;
#116=AXIS2_PLACEMENT_3D ( 'NONE', #21705, #19183, #32879 ) ;
#121=CARTESIAN_POINT ( 'NONE',  ( 8.000000000000000000, -6.085920226790910270, -15.78165944574524637 ) ) ;
#127=DIRECTION ( 'NONE',  ( 0.000000000000000000, 0.000000000000000000, 1.000000000000000000 ) ) ;
#142=EDGE_LOOP ( 'NONE', ( #28421, #17559, #31221, #701 ) ) ;
#146=EDGE_LOOP ( 'NONE', ( #18691, #20967, #34067, #15002, #19215, #15839 ) ) ;
#148=AXIS2_PLACEMENT_3D ( 'NONE', #26646, #23213, #28979 ) ;
#153=CARTESIAN_POINT ( 'NONE',  ( 8.000000000000000000, 8.605879768205236147, 12.89022243466711615 ) ) ;
#176=CARTESIAN_POINT ( 'NONE',  ( 8.000000000000000000, 5.482169781019050170, -16.00140663693117560 ) ) ;
#192=VERTEX_POINT ( 'NONE', #6754 ) ;
#196=LINE ( 'NONE', #5955, #10522 ) ;
#206=EDGE_LOOP ( 'NONE', ( #28394, #8003, #20134, #21793 ) ) ;
#207=DIRECTION ( 'NONE',  ( 0.000000000000000000, 0.000000000000000000, 1.000000000000000000 ) ) ;
#208=CARTESIAN_POINT ( 'NONE',  ( 8.000000000000000000, 0.000000000000000000, 20.00000000000000000 ) ) ;
#211=VERTEX_POINT ( 'NONE', #18081 ) ;
#217=ADVANCED_FACE ( 'NONE', ( #9811 ), #28733, .T. ) ;
#241=EDGE_CURVE ( 'NONE', #27557, #21748, #15191, .T. ) ;
#268=ORIENTED_EDGE ( 'NONE', *, *, #6401, .F. ) ;
#274=EDGE_CURVE ( 'NONE', #16735, #21654, #4432, .T. ) ;
#306=DIRECTION ( 'NONE',  ( -1.000000000000000000, 0.000000000000000000, 0.000000000000000000 ) ) ;
#322=DIRECTION ( 'NONE',  ( 0.000000000000000000, 0.6427876096865349220, 0.7660444431189816772 ) ) ;
#333=DIRECTION ( 'NONE',  ( -1.000000000000000000, 0.000000000000000000, 0.000000000000000000 ) ) ;
#335=DIRECTION ( 'NONE',  ( -1.000000000000000000, 0.000000000000000000, 0.000000000000000000 ) ) ;
#372=AXIS2_PLACEMENT_3D ( 'NONE', #3017, #13976, #33249 ) ;
#378=CYLINDRICAL_SURFACE ( 'NONE', #30091, 15.49899999999998457 ) ;
#384=VECTOR ( 'NONE', #23234, 1000.000000000000000 ) ;
#393=CYLINDRICAL_SURFACE ( 'NONE', #30281, 7.199999999999993072 ) ;
#398=AXIS2_PLACEMENT_3D ( 'NONE', #35095, #21378, #5020 ) ;
#400=EDGE_CURVE ( 'NONE', #22707, #21695, #5318, .T. ) ;
#408=PRODUCT_DEFINITION_CONTEXT ( 'detailed design', #15835, 'design' ) ;
#421=CARTESIAN_POINT ( 'NONE',  ( 8.000000000000000000, 1.693188892523948885, -15.40623615209870323 ) ) ;
#444=DIRECTION ( 'NONE',  ( -1.000000000000000000, 0.000000000000000000, 0.000000000000000000 ) ) ;
#448=EDGE_CURVE ( 'NONE', #932, #28254, #34663, .T. ) ;
#449=ORIENTED_EDGE ( 'NONE', *, *, #1744, .T. ) ;
#459=CARTESIAN_POINT ( 'NONE',  ( 8.000000000000000000, 10.62435788049443808, 13.16139124467922272 ) ) ;
#465=DIRECTION ( 'NONE',  ( 1.000000000000000000, -0.000000000000000000, 0.000000000000000000 ) ) ;
#527=ORIENTED_EDGE ( 'NONE', *, *, #11411, .F. ) ;
#533=DIRECTION ( 'NONE',  ( -1.000000000000000000, 0.000000000000000000, 0.000000000000000000 ) ) ;
#537=CARTESIAN_POINT ( 'NONE',  ( 0.000000000000000000, 0.000000000000000000, 0.000000000000000000 ) ) ;
#549=DIRECTION ( 'NONE',  ( -1.000000000000000000, 0.000000000000000000, 0.000000000000000000 ) ) ;
#586=CARTESIAN_POINT ( 'NONE',  ( 8.000000000000000000, 3.678165988948789877, -15.05623113391063406 ) ) ;
#596=DIRECTION ( 'NONE',  ( -1.000000000000000000, 0.000000000000000000, 0.000000000000000000 ) ) ;
#598=AXIS2_PLACEMENT_3D ( 'NONE', #31782, #23685, #21325 ) ;
#599=AXIS2_PLACEMENT_3D ( 'NONE', #5420, #533, #19441 ) ;
#637=EDGE_CURVE ( 'NONE', #14516, #4854, #18566, .T. ) ;
#641=CARTESIAN_POINT ( 'NONE',  ( 50.00005079999999680, 5.400000000000000355, -0.9999999999999985567 ) ) ;
#650=DIRECTION ( 'NONE',  ( -1.000000000000000000, 0.000000000000000000, 0.000000000000000000 ) ) ;
#652=ORIENTED_EDGE ( 'NONE', *, *, #8841, .T. ) ;
#656=VERTEX_POINT ( 'NONE', #964 ) ;
#663=ORIENTED_EDGE ( 'NONE', *, *, #14067, .F. ) ;
#670=CIRCLE ( 'NONE', #8717, 15.49899999999998457 ) ;
#674=CARTESIAN_POINT ( 'NONE',  ( 8.000000000000000000, 0.3212489022567689423, -16.91141623315866482 ) ) ;
#683=AXIS2_PLACEMENT_3D ( 'NONE', #6567, #26384, #18080 ) ;
#684=FACE_OUTER_BOUND ( 'NONE', #26041, .T. ) ;
#695=DIRECTION ( 'NONE',  ( -1.000000000000000000, 0.000000000000000000, 0.000000000000000000 ) ) ;
#696=ORIENTED_EDGE ( 'NONE', *, *, #4802, .T. ) ;
#701=ORIENTED_EDGE ( 'NONE', *, *, #8316, .T. ) ;
#711=ADVANCED_FACE ( 'NONE', ( #28693 ), #34457, .F. ) ;
#714=EDGE_CURVE ( 'NONE', #28345, #33371, #20371, .T. ) ;
#723=CARTESIAN_POINT ( 'NONE',  ( 8.000000000000000000, 0.000000000000000000, 0.000000000000000000 ) ) ;
#754=CARTESIAN_POINT ( 'NONE',  ( 0.000000000000000000, 0.000000000000000000, 0.000000000000000000 ) ) ;
#756=ORIENTED_EDGE ( 'NONE', *, *, #11411, .T. ) ;
#758=CARTESIAN_POINT ( 'NONE',  ( 0.000000000000000000, 16.59870953437680896, 3.253005020243904255 ) ) ;
#765=AXIS2_PLACEMENT_3D ( 'NONE', #10520, #29975, #33023 ) ;
#823=CARTESIAN_POINT ( 'NONE',  ( 0.000000000000000000, 0.000000000000000000, 0.000000000000000000 ) ) ;
#840=EDGE_LOOP ( 'NONE', ( #34397, #4739, #23398, #35409 ) ) ;
#856=LINE ( 'NONE', #14891, #34928 ) ;
#876=VERTEX_POINT ( 'NONE', #27238 ) ;
#878=EDGE_CURVE ( 'NONE', #32697, #33707, #24177, .T. ) ;
#889=DIRECTION ( 'NONE',  ( -1.000000000000000000, 0.000000000000000000, 0.000000000000000000 ) ) ;
#890=AXIS2_PLACEMENT_3D ( 'NONE', #13160, #26663, #24135 ) ;
#905=AXIS2_PLACEMENT_3D ( 'NONE', #14826, #14455, #1154 ) ;
#914=EDGE_LOOP ( 'NONE', ( #16361, #32759, #8268, #34150 ) ) ;
#932=VERTEX_POINT ( 'NONE', #34998 ) ;
#934=LINE ( 'NONE', #18017, #26319 ) ;
#943=CARTESIAN_POINT ( 'NONE',  ( 8.000000000000000000, -16.71027810728550733, -2.620268201066114688 ) ) ;
#947=ADVANCED_FACE ( 'NONE', ( #11026 ), #32450, .T. ) ;
#964=CARTESIAN_POINT ( 'NONE',  ( 8.000000000000000000, 19.60123832284017453, 3.973846525876499225 ) ) ;
#984=VERTEX_POINT ( 'NONE', #11377 ) ;
#985=ORIENTED_EDGE ( 'NONE', *, *, #1744, .F. ) ;
#1026=VERTEX_POINT ( 'NONE', #28115 ) ;
#1027=AXIS2_PLACEMENT_3D ( 'NONE', #29683, #9873, #7366 ) ;
#1038=VECTOR ( 'NONE', #35170, 1000.000000000000000 ) ;
#1040=ORIENTED_EDGE ( 'NONE', *, *, #17483, .T. ) ;
#1075=AXIS2_PLACEMENT_3D ( 'NONE', #10480, #13193, #34986 ) ;
#1090=LINE ( 'NONE', #12782, #18845 ) ;
#1101=VERTEX_POINT ( 'NONE', #208 ) ;
#1103=ORIENTED_EDGE ( 'NONE', *, *, #15865, .T. ) ;
#1106=EDGE_CURVE ( 'NONE', #7183, #1299, #2524, .T. ) ;
#1109=ORIENTED_EDGE ( 'NONE', *, *, #2269, .F. ) ;
#1119=DIRECTION ( 'NONE',  ( -1.000000000000000000, 0.000000000000000000, 0.000000000000000000 ) ) ;
#1147=ADVANCED_FACE ( 'NONE', ( #33679 ), #378, .T. ) ;
#1151=AXIS2_PLACEMENT_3D ( 'NONE', #25870, #19708, #17195 ) ;
#1154=DIRECTION ( 'NONE',  ( 0.000000000000000000, 0.000000000000000000, 1.000000000000000000 ) ) ;
#1157=DIRECTION ( 'NONE',  ( -1.000000000000000000, 0.000000000000000000, 0.000000000000000000 ) ) ;
#1172=CYLINDRICAL_SURFACE ( 'NONE', #34649, 19.99999999999998579 ) ;
#1176=EDGE_CURVE ( 'NONE', #9468, #31771, #34225, .T. ) ;
#1178=CIRCLE ( 'NONE', #25910, 3.999999999999996447 ) ;
#1198=DIRECTION ( 'NONE',  ( 0.000000000000000000, 0.000000000000000000, 1.000000000000000000 ) ) ;
#1205=AXIS2_PLACEMENT_3D ( 'NONE', #29045, #1500, #20744 ) ;
#1206=CIRCLE ( 'NONE', #18435, 3.999999999999996447 ) ;
#1211=CARTESIAN_POINT ( 'NONE',  ( 4.000000000000000000, 6.359167119270718871, -18.96209359615085788 ) ) ;
#1215=ORIENTED_EDGE ( 'NONE', *, *, #24076, .F. ) ;
#1229=( GEOMETRIC_REPRESENTATION_CONTEXT ( 3 ) GLOBAL_UNCERTAINTY_ASSIGNED_CONTEXT ( ( #20365 ) ) GLOBAL_UNIT_ASSIGNED_CONTEXT ( ( #10687, #18958, #29954 ) ) REPRESENTATION_CONTEXT ( 'NONE', 'WORKASPACE' ) );
#1241=VERTEX_POINT ( 'NONE', #31342 ) ;
#1246=EDGE_CURVE ( 'NONE', #16735, #21743, #18612, .T. ) ;
#1247=FACE_OUTER_BOUND ( 'NONE', #24776, .T. ) ;
#1263=DIRECTION ( 'NONE',  ( -1.000000000000000000, 0.000000000000000000, 0.000000000000000000 ) ) ;
#1273=CIRCLE ( 'NONE', #116, 15.49899999999999700 ) ;
#1284=FACE_OUTER_BOUND ( 'NONE', #24156, .T. ) ;
#1288=ORIENTED_EDGE ( 'NONE', *, *, #21239, .T. ) ;
#1299=VERTEX_POINT ( 'NONE', #9914 ) ;
#1312=VECTOR ( 'NONE', #33377, 1000.000000000000000 ) ;
#1327=CARTESIAN_POINT ( 'NONE',  ( 8.000000000000000000, 0.000000000000000000, 0.000000000000000000 ) ) ;
#1332=ORIENTED_EDGE ( 'NONE', *, *, #34804, .T. ) ;
#1342=EDGE_CURVE ( 'NONE', #27693, #32697, #31262, .T. ) ;
#1385=SHAPE_DEFINITION_REPRESENTATION ( #19819, #11863 ) ;
#1391=DIRECTION ( 'NONE',  ( 0.000000000000000000, 0.000000000000000000, 1.000000000000000000 ) ) ;
#1410=ADVANCED_FACE ( 'NONE', ( #2372, #2728 ), #32242, .F. ) ;
#1420=ORIENTED_EDGE ( 'NONE', *, *, #10163, .F. ) ;
#1424=ORIENTED_EDGE ( 'NONE', *, *, #13704, .F. ) ;
#1439=DIRECTION ( 'NONE',  ( 0.000000000000000000, 0.8660254037844398178, -0.4999999999999980571 ) ) ;
#1452=VERTEX_POINT ( 'NONE', #26851 ) ;
#1454=ORIENTED_EDGE ( 'NONE', *, *, #21547, .T. ) ;
#1478=ORIENTED_EDGE ( 'NONE', *, *, #22705, .T. ) ;
#1479=ORIENTED_EDGE ( 'NONE', *, *, #4647, .F. ) ;
#1485=DIRECTION ( 'NONE',  ( -1.000000000000000000, 0.000000000000000000, 0.000000000000000000 ) ) ;
#1500=DIRECTION ( 'NONE',  ( -1.000000000000000000, 0.000000000000000000, 0.000000000000000000 ) ) ;
#1504=DIRECTION ( 'NONE',  ( 0.000000000000000000, 0.3420201433256629953, 0.9396926207859104263 ) ) ;
#1520=CARTESIAN_POINT ( 'NONE',  ( 8.000000000000000000, 0.000000000000000000, 0.000000000000000000 ) ) ;
#1542=CYLINDRICAL_SURFACE ( 'NONE', #10178, 7.199999999999994849 ) ;
#1581=CIRCLE ( 'NONE', #34352, 3.999999999999996447 ) ;
#1583=EDGE_CURVE ( 'NONE', #5158, #6999, #31846, .T. ) ;
#1605=VERTEX_POINT ( 'NONE', #22130 ) ;
#1607=ORIENTED_EDGE ( 'NONE', *, *, #400, .T. ) ;
#1620=EDGE_CURVE ( 'NONE', #12194, #27370, #6107, .T. ) ;
#1621=DIRECTION ( 'NONE',  ( -1.000000000000000000, 0.000000000000000000, 0.000000000000000000 ) ) ;
#1633=LINE ( 'NONE', #15813, #6328 ) ;
#1638=ORIENTED_EDGE ( 'NONE', *, *, #29883, .T. ) ;
#1641=CIRCLE ( 'NONE', #34441, 7.199999999999995737 ) ;
#1645=VERTEX_POINT ( 'NONE', #27562 ) ;
#1679=ORIENTED_EDGE ( 'NONE', *, *, #12599, .T. ) ;
#1688=DIRECTION ( 'NONE',  ( 0.000000000000000000, -0.8660254037844329345, -0.5000000000000101030 ) ) ;
#1713=ORIENTED_EDGE ( 'NONE', *, *, #14111, .F. ) ;
#1714=AXIS2_PLACEMENT_3D ( 'NONE', #11283, #19375, #10758 ) ;
#1720=DIRECTION ( 'NONE',  ( -1.000000000000000000, 0.000000000000000000, 0.000000000000000000 ) ) ;
#1733=( LENGTH_UNIT ( ) NAMED_UNIT ( * ) SI_UNIT ( .MILLI., .METRE. ) );
#1736=CIRCLE ( 'NONE', #13264, 19.99999999999998579 ) ;
#1741=AXIS2_PLACEMENT_3D ( 'NONE', #11264, #14475, #33059 ) ;
#1744=EDGE_CURVE ( 'NONE', #4405, #6685, #15744, .T. ) ;
#1754=EDGE_LOOP ( 'NONE', ( #33184, #22637, #28342, #32874 ) ) ;
#1757=DIRECTION ( 'NONE',  ( -1.000000000000000000, 0.000000000000000000, 0.000000000000000000 ) ) ;
#1766=ADVANCED_BREP_SHAPE_REPRESENTATION ( '', ( #34287, #21307 ), #1229 ) ;
#1795=ORIENTED_EDGE ( 'NONE', *, *, #17528, .T. ) ;
#1810=DIRECTION ( 'NONE',  ( -1.000000000000000000, 0.000000000000000000, 0.000000000000000000 ) ) ;
#1818=ORIENTED_EDGE ( 'NONE', *, *, #35286, .F. ) ;
#1823=CARTESIAN_POINT ( 'NONE',  ( 0.000000000000000000, 0.000000000000000000, 0.000000000000000000 ) ) ;
#1840=ORIENTED_EDGE ( 'NONE', *, *, #5603, .T. ) ;
#1851=ORIENTED_EDGE ( 'NONE', *, *, #2245, .F. ) ;
#1923=CARTESIAN_POINT ( 'NONE',  ( 50.00005079999999680, 0.000000000000000000, 3.999999999999996447 ) ) ;
#1950=DIRECTION ( 'NONE',  ( -1.000000000000000000, 0.000000000000000000, 0.000000000000000000 ) ) ;
#1963=EDGE_LOOP ( 'NONE', ( #1818, #33515, #756, #19170 ) ) ;
#1973=ORIENTED_EDGE ( 'NONE', *, *, #5562, .T. ) ;
#1981=EDGE_CURVE ( 'NONE', #18606, #26760, #7528, .T. ) ;
#1982=CARTESIAN_POINT ( 'NONE',  ( 8.000000000000000000, -14.18878633068163708, 6.236773481718040024 ) ) ;
#1986=CARTESIAN_POINT ( 'NONE',  ( 0.000000000000000000, 0.000000000000000000, 0.000000000000000000 ) ) ;
#1994=CARTESIAN_POINT ( 'NONE',  ( 0.000000000000000000, -15.46619997295644033, 1.007799283846635863 ) ) ;
#1996=ORIENTED_EDGE ( 'NONE', *, *, #26272, .F. ) ;
#2021=CIRCLE ( 'NONE', #6590, 7.199999999999994849 ) ;
#2032=CIRCLE ( 'NONE', #12365, 7.199999999999993960 ) ;
#2062=ORIENTED_EDGE ( 'NONE', *, *, #18309, .T. ) ;
#2066=FILL_AREA_STYLE_COLOUR ( '', #21340 ) ;
#2068=ORIENTED_EDGE ( 'NONE', *, *, #14371, .T. ) ;
#2071=DIRECTION ( 'NONE',  ( -1.000000000000000000, 0.000000000000000000, 0.000000000000000000 ) ) ;
#2082=CARTESIAN_POINT ( 'NONE',  ( 0.000000000000000000, 0.000000000000000000, 0.000000000000000000 ) ) ;
#2083=CIRCLE ( 'NONE', #15818, 3.999999999999996447 ) ;
#2106=VERTEX_POINT ( 'NONE', #22608 ) ;
#2114=ORIENTED_EDGE ( 'NONE', *, *, #23354, .F. ) ;
#2125=ADVANCED_FACE ( 'NONE', ( #13990 ), #27692, .T. ) ;
#2176=DIRECTION ( 'NONE',  ( -1.000000000000000000, 0.000000000000000000, 0.000000000000000000 ) ) ;
#2178=AXIS2_PLACEMENT_3D ( 'NONE', #35388, #16804, #8534 ) ;
#2196=ORIENTED_EDGE ( 'NONE', *, *, #2411, .T. ) ;
#2198=CARTESIAN_POINT ( 'NONE',  ( 8.000000000000000000, -16.59870953437682672, 3.253005020243791456 ) ) ;
#2211=VERTEX_POINT ( 'NONE', #33087 ) ;
#2242=FACE_OUTER_BOUND ( 'NONE', #30179, .T. ) ;
#2245=EDGE_CURVE ( 'NONE', #13869, #27693, #12180, .T. ) ;
#2252=AXIS2_PLACEMENT_3D ( 'NONE', #10917, #4983, #24777 ) ;
#2254=DIRECTION ( 'NONE',  ( 0.000000000000000000, 0.000000000000000000, -1.000000000000000000 ) ) ;
#2263=CARTESIAN_POINT ( 'NONE',  ( 0.000000000000000000, 0.5097555531875970214, -19.99350267651952606 ) ) ;
#2269=EDGE_CURVE ( 'NONE', #8899, #20033, #2601, .T. ) ;
#2295=ORIENTED_EDGE ( 'NONE', *, *, #1583, .T. ) ;
#2296=EDGE_CURVE ( 'NONE', #31709, #31717, #8888, .T. ) ;
#2307=DIRECTION ( 'NONE',  ( 0.000000000000000000, 0.000000000000000000, 1.000000000000000000 ) ) ;
#2318=DIRECTION ( 'NONE',  ( -1.000000000000000000, 0.000000000000000000, 0.000000000000000000 ) ) ;
#2326=CARTESIAN_POINT ( 'NONE',  ( 8.000000000000000000, 0.000000000000000000, 0.000000000000000000 ) ) ;
#2372=FACE_OUTER_BOUND ( 'NONE', #14967, .T. ) ;
#2374=ORIENTED_EDGE ( 'NONE', *, *, #11027, .F. ) ;
#2402=( GEOMETRIC_REPRESENTATION_CONTEXT ( 3 ) GLOBAL_UNCERTAINTY_ASSIGNED_CONTEXT ( ( #2802 ) ) GLOBAL_UNIT_ASSIGNED_CONTEXT ( ( #29781, #13389, #18603 ) ) REPRESENTATION_CONTEXT ( 'NONE', 'WORKASPACE' ) );
#2408=EDGE_CURVE ( 'NONE', #7160, #28086, #34768, .T. ) ;
#2411=EDGE_CURVE ( 'NONE', #26625, #9040, #7308, .T. ) ;
#2414=ORIENTED_EDGE ( 'NONE', *, *, #14799, .T. ) ;
#2425=CARTESIAN_POINT ( 'NONE',  ( 4.000000000000000000, 19.77827456857338007, -2.969824084036535528 ) ) ;
#2444=ORIENTED_EDGE ( 'NONE', *, *, #21190, .T. ) ;
#2455=EDGE_LOOP ( 'NONE', ( #24664, #34048, #10957, #30998 ) ) ;
#2466=ORIENTED_EDGE ( 'NONE', *, *, #33726, .F. ) ;
#2482=EDGE_CURVE ( 'NONE', #16891, #15563, #13430, .T. ) ;
#2485=DIRECTION ( 'NONE',  ( -1.000000000000000000, 0.000000000000000000, 0.000000000000000000 ) ) ;
#2493=ADVANCED_FACE ( 'NONE', ( #24411 ), #35398, .T. ) ;
#2499=ORIENTED_EDGE ( 'NONE', *, *, #4647, .T. ) ;
#2505=AXIS2_PLACEMENT_3D ( 'NONE', #32867, #8544, #33045 ) ;
#2508=CARTESIAN_POINT ( 'NONE',  ( 0.000000000000000000, 14.48509162075963985, 8.733917826871412160 ) ) ;
#2524=CIRCLE ( 'NONE', #24921, 7.199999999999998401 ) ;
#2527=EDGE_CURVE ( 'NONE', #10299, #10915, #31973, .T. ) ;
#2534=ORIENTED_EDGE ( 'NONE', *, *, #1620, .T. ) ;
#2542=ADVANCED_FACE ( 'NONE', ( #25294 ), #5851, .T. ) ;
#2543=FACE_OUTER_BOUND ( 'NONE', #19549, .T. ) ;
#2544=VERTEX_POINT ( 'NONE', #5505 ) ;
#2552=DIRECTION ( 'NONE',  ( -1.000000000000000000, 0.000000000000000000, 0.000000000000000000 ) ) ;
#2581=CARTESIAN_POINT ( 'NONE',  ( 4.000000000000000000, -6.359167119270592750, 18.96209359615092183 ) ) ;
#2590=ORIENTED_EDGE ( 'NONE', *, *, #20513, .T. ) ;
#2594=ORIENTED_EDGE ( 'NONE', *, *, #8316, .F. ) ;
#2601=CIRCLE ( 'NONE', #26731, 7.199999999999998401 ) ;
#2606=ADVANCED_FACE ( 'NONE', ( #8190 ), #11596, .T. ) ;
#2613=DIRECTION ( 'NONE',  ( -1.000000000000000000, 0.000000000000000000, 0.000000000000000000 ) ) ;
#2652=CARTESIAN_POINT ( 'NONE',  ( 8.000000000000000000, 0.000000000000000000, 0.000000000000000000 ) ) ;
#2666=LINE ( 'NONE', #19195, #34893 ) ;
#2668=LINE ( 'NONE', #30545, #14166 ) ;
#2683=AXIS2_PLACEMENT_3D ( 'NONE', #10663, #10846, #35164 ) ;
#2689=AXIS2_PLACEMENT_3D ( 'NONE', #10908, #18996, #7832 ) ;
#2696=EDGE_CURVE ( 'NONE', #21748, #18374, #15700, .T. ) ;
#2710=AXIS2_PLACEMENT_3D ( 'NONE', #15922, #29091, #26393 ) ;
#2712=CARTESIAN_POINT ( 'NONE',  ( 0.000000000000000000, 3.872983346207417021, 0.9999999999999985567 ) ) ;
#2725=ORIENTED_EDGE ( 'NONE', *, *, #5182, .F. ) ;
#2726=ORIENTED_EDGE ( 'NONE', *, *, #6928, .F. ) ;
#2728=FACE_BOUND ( 'NONE', #146, .T. ) ;
#2733=DIRECTION ( 'NONE',  ( -1.000000000000000000, 0.000000000000000000, 0.000000000000000000 ) ) ;
#2747=CIRCLE ( 'NONE', #10168, 15.49900000000000233 ) ;
#2794=DIRECTION ( 'NONE',  ( 0.000000000000000000, 0.6427876096865403621, -0.7660444431189772363 ) ) ;
#2797=CYLINDRICAL_SURFACE ( 'NONE', #16693, 7.199999999999994849 ) ;
#2802=UNCERTAINTY_MEASURE_WITH_UNIT (LENGTH_MEASURE( 1.000000000000000082E-05 ), #29781, 'distance_accuracy_value', 'NONE');
#2814=CARTESIAN_POINT ( 'NONE',  ( 0.000000000000000000, 13.24207120356986422, -14.98824707027428005 ) ) ;
#2822=EDGE_CURVE ( 'NONE', #11394, #4405, #32374, .T. ) ;
#2841=CARTESIAN_POINT ( 'NONE',  ( 4.000000000000000000, -0.5097555531871980072, -19.99350267651955804 ) ) ;
#2849=ORIENTED_EDGE ( 'NONE', *, *, #24871, .F. ) ;
#2859=ORIENTED_EDGE ( 'NONE', *, *, #16384, .F. ) ;
#2865=CARTESIAN_POINT ( 'NONE',  ( 0.000000000000000000, 0.000000000000000000, 0.000000000000000000 ) ) ;
#2879=LINE ( 'NONE', #153, #33543 ) ;
#2891=CIRCLE ( 'NONE', #14930, 7.199999999999991296 ) ;
#2894=DIRECTION ( 'NONE',  ( 0.000000000000000000, -0.8660254037844327124, -0.5000000000000101030 ) ) ;
#2896=VERTEX_POINT ( 'NONE', #9612 ) ;
#2918=CIRCLE ( 'NONE', #599, 19.99999999999998579 ) ;
#2926=EDGE_CURVE ( 'NONE', #26998, #31709, #11771, .T. ) ;
#2955=DIRECTION ( 'NONE',  ( 0.000000000000000000, 0.000000000000000000, 1.000000000000000000 ) ) ;
#2961=LINE ( 'NONE', #586, #6281 ) ;
#2985=EDGE_CURVE ( 'NONE', #24079, #15022, #11695, .T. ) ;
#2992=DIRECTION ( 'NONE',  ( 0.000000000000000000, 0.000000000000000000, -1.000000000000000000 ) ) ;
#2996=CIRCLE ( 'NONE', #22511, 19.99999999999998579 ) ;
#2999=EDGE_LOOP ( 'NONE', ( #33499, #12810, #10509, #20341 ) ) ;
#3014=AXIS2_PLACEMENT_3D ( 'NONE', #459, #28008, #25304 ) ;
#3017=CARTESIAN_POINT ( 'NONE',  ( 0.000000000000000000, -14.80634052301617309, -8.177498406287382338 ) ) ;
#3029=CARTESIAN_POINT ( 'NONE',  ( 8.000000000000000000, 0.000000000000000000, 0.000000000000000000 ) ) ;
#3034=DIRECTION ( 'NONE',  ( -1.000000000000000000, 0.000000000000000000, 0.000000000000000000 ) ) ;
#3036=DIRECTION ( 'NONE',  ( -1.000000000000000000, 0.000000000000000000, 0.000000000000000000 ) ) ;
#3046=EDGE_CURVE ( 'NONE', #30129, #2544, #14561, .T. ) ;
#3054=CARTESIAN_POINT ( 'NONE',  ( 8.000000000000000000, -6.359167119270333401, -18.96209359615098577 ) ) ;
#3055=DIRECTION ( 'NONE',  ( -1.000000000000000000, 0.000000000000000000, 0.000000000000000000 ) ) ;
#3074=AXIS2_PLACEMENT_3D ( 'NONE', #18258, #29261, #14847 ) ;
#3100=CIRCLE ( 'NONE', #11135, 7.199999999999993960 ) ;
#3107=EDGE_CURVE ( 'NONE', #10099, #28443, #12794, .T. ) ;
#3110=ORIENTED_EDGE ( 'NONE', *, *, #18733, .T. ) ;
#3120=ORIENTED_EDGE ( 'NONE', *, *, #29084, .F. ) ;
#3161=ORIENTED_EDGE ( 'NONE', *, *, #26875, .F. ) ;
#3170=EDGE_CURVE ( 'NONE', #26059, #1241, #21974, .T. ) ;
#3195=DIRECTION ( 'NONE',  ( 0.000000000000000000, -6.987080667128811962E-15, 1.000000000000000000 ) ) ;
#3204=ORIENTED_EDGE ( 'NONE', *, *, #13737, .T. ) ;
#3207=DIRECTION ( 'NONE',  ( -1.000000000000000000, 0.000000000000000000, 0.000000000000000000 ) ) ;
#3212=FACE_OUTER_BOUND ( 'NONE', #3730, .T. ) ;
#3237=CARTESIAN_POINT ( 'NONE',  ( 0.000000000000000000, 0.000000000000000000, 0.000000000000000000 ) ) ;
#3242=AXIS2_PLACEMENT_3D ( 'NONE', #11628, #16673, #22601 ) ;
#3246=CIRCLE ( 'NONE', #9587, 7.199999999999994849 ) ;
#3283=CYLINDRICAL_SURFACE ( 'NONE', #10160, 7.199999999999994849 ) ;
#3287=CARTESIAN_POINT ( 'NONE',  ( 8.000000000000000000, -12.49559743815785140, 9.169462670380546854 ) ) ;
#3299=AXIS2_PLACEMENT_3D ( 'NONE', #28734, #34852, #23679 ) ;
#3303=DIRECTION ( 'NONE',  ( -1.000000000000000000, 0.000000000000000000, 0.000000000000000000 ) ) ;
#3331=CARTESIAN_POINT ( 'NONE',  ( 0.000000000000000000, -16.59870953437682672, 3.253005020243791456 ) ) ;
#3347=ADVANCED_FACE ( 'NONE', ( #5093, #24345 ), #18397, .F. ) ;
#3348=ORIENTED_EDGE ( 'NONE', *, *, #35246, .T. ) ;
#3381=CARTESIAN_POINT ( 'NONE',  ( 0.000000000000000000, 5.400000000000000355, -0.9999999999999985567 ) ) ;
#3398=ORIENTED_EDGE ( 'NONE', *, *, #11251, .T. ) ;
#3405=CARTESIAN_POINT ( 'NONE',  ( 0.000000000000000000, 0.000000000000000000, 0.000000000000000000 ) ) ;
#3406=CARTESIAN_POINT ( 'NONE',  ( 8.000000000000000000, 0.000000000000000000, 0.000000000000000000 ) ) ;
#3461=CARTESIAN_POINT ( 'NONE',  ( 0.000000000000000000, -19.77827456857333743, -2.969824084036672751 ) ) ;
#3476=CIRCLE ( 'NONE', #26479, 19.99999999999998579 ) ;
#3512=DIRECTION ( 'NONE',  ( 0.000000000000000000, 0.6427876096865349220, 0.7660444431189816772 ) ) ;
#3521=AXIS2_PLACEMENT_3D ( 'NONE', #24715, #43, #13207 ) ;
#3526=DIRECTION ( 'NONE',  ( -1.000000000000000000, 0.000000000000000000, 0.000000000000000000 ) ) ;
#3532=EDGE_CURVE ( 'NONE', #26843, #30129, #196, .T. ) ;
#3540=CARTESIAN_POINT ( 'NONE',  ( 8.000000000000000000, 14.80634052301623171, 8.177498406287277533 ) ) ;
#3583=DIRECTION ( 'NONE',  ( 0.000000000000000000, 0.000000000000000000, 1.000000000000000000 ) ) ;
#3586=CARTESIAN_POINT ( 'NONE',  ( 0.000000000000000000, 6.359167119270718871, -18.96209359615085788 ) ) ;
#3612=ADVANCED_FACE ( 'NONE', ( #11882 ), #12247, .T. ) ;
#3615=VERTEX_POINT ( 'NONE', #23037 ) ;
#3623=EDGE_CURVE ( 'NONE', #2106, #1101, #17984, .T. ) ;
#3628=DIRECTION ( 'NONE',  ( -1.000000000000000000, 0.000000000000000000, 0.000000000000000000 ) ) ;
#3633=DIRECTION ( 'NONE',  ( -1.000000000000000000, 0.000000000000000000, 0.000000000000000000 ) ) ;
#3658=FACE_OUTER_BOUND ( 'NONE', #14381, .T. ) ;
#3679=DIRECTION ( 'NONE',  ( 0.000000000000000000, -8.881784197001252323E-16, -1.000000000000000000 ) ) ;
#3686=DIRECTION ( 'NONE',  ( -1.000000000000000000, 0.000000000000000000, 0.000000000000000000 ) ) ;
#3700=FACE_OUTER_BOUND ( 'NONE', #2999, .T. ) ;
#3728=ORIENTED_EDGE ( 'NONE', *, *, #2296, .F. ) ;
#3730=EDGE_LOOP ( 'NONE', ( #22010, #30073, #1288, #5060 ) ) ;
#3749=DIRECTION ( 'NONE',  ( 0.000000000000000000, 0.000000000000000000, 1.000000000000000000 ) ) ;
#3758=CARTESIAN_POINT ( 'NONE',  ( 8.000000000000000000, 0.000000000000000000, 0.000000000000000000 ) ) ;
#3762=ORIENTED_EDGE ( 'NONE', *, *, #12646, .F. ) ;
#3804=AXIS2_PLACEMENT_3D ( 'NONE', #1823, #23779, #5412 ) ;
#3812=EDGE_CURVE ( 'NONE', #3615, #10084, #34695, .T. ) ;
#3825=EDGE_LOOP ( 'NONE', ( #652, #9347, #9995, #31273 ) ) ;
#3851=DIRECTION ( 'NONE',  ( 1.000000000000000000, -0.000000000000000000, 0.000000000000000000 ) ) ;
#3867=CARTESIAN_POINT ( 'NONE',  ( 4.000000000000000000, 12.46108038583334299, -15.64357617738982142 ) ) ;
#3874=EDGE_LOOP ( 'NONE', ( #8444, #34699, #31317, #17340 ) ) ;
#3902=DIRECTION ( 'NONE',  ( -1.000000000000000000, 0.000000000000000000, 0.000000000000000000 ) ) ;
#3908=VECTOR ( 'NONE', #33852, 1000.000000000000000 ) ;
#3916=AXIS2_PLACEMENT_3D ( 'NONE', #21919, #30216, #27526 ) ;
#3921=EDGE_CURVE ( 'NONE', #31804, #24979, #4867, .T. ) ;
#3939=FACE_OUTER_BOUND ( 'NONE', #23878, .T. ) ;
#3947=VECTOR ( 'NONE', #24632, 1000.000000000000000 ) ;
#3980=EDGE_CURVE ( 'NONE', #26953, #19119, #24653, .T. ) ;
#3982=DIRECTION ( 'NONE',  ( -1.000000000000000000, 0.000000000000000000, 0.000000000000000000 ) ) ;
#4001=DIRECTION ( 'NONE',  ( 0.000000000000000000, 0.000000000000000000, 1.000000000000000000 ) ) ;
#4002=VERTEX_POINT ( 'NONE', #8601 ) ;
#4022=AXIS2_PLACEMENT_3D ( 'NONE', #15964, #23913, #4302 ) ;
#4062=VERTEX_POINT ( 'NONE', #5398 ) ;
#4065=CARTESIAN_POINT ( 'NONE',  ( 8.000000000000000000, 14.48509162075963985, 8.733917826871412160 ) ) ;
#4066=EDGE_CURVE ( 'NONE', #17047, #11373, #2879, .T. ) ;
#4088=DIRECTION ( 'NONE',  ( 0.000000000000000000, 0.000000000000000000, 1.000000000000000000 ) ) ;
#4110=ORIENTED_EDGE ( 'NONE', *, *, #7792, .F. ) ;
#4128=CARTESIAN_POINT ( 'NONE',  ( 0.000000000000000000, -8.605879768205326741, 12.89022243466705930 ) ) ;
#4130=ORIENTED_EDGE ( 'NONE', *, *, #12569, .F. ) ;
#4165=ORIENTED_EDGE ( 'NONE', *, *, #28596, .T. ) ;
#4176=ORIENTED_EDGE ( 'NONE', *, *, #30877, .T. ) ;
#4192=ORIENTED_EDGE ( 'NONE', *, *, #26875, .T. ) ;
#4223=DIRECTION ( 'NONE',  ( 0.000000000000000000, 0.8660254037844364872, 0.5000000000000036637 ) ) ;
#4230=ORIENTED_EDGE ( 'NONE', *, *, #20513, .F. ) ;
#4238=EDGE_CURVE ( 'NONE', #18735, #11499, #5355, .T. ) ;
#4248=CARTESIAN_POINT ( 'NONE',  ( 0.000000000000000000, 0.000000000000000000, 0.000000000000000000 ) ) ;
#4254=DIRECTION ( 'NONE',  ( 0.000000000000000000, 0.000000000000000000, 1.000000000000000000 ) ) ;
#4264=DIRECTION ( 'NONE',  ( -1.000000000000000000, 0.000000000000000000, 0.000000000000000000 ) ) ;
#4284=ORIENTED_EDGE ( 'NONE', *, *, #20246, .F. ) ;
#4301=CARTESIAN_POINT ( 'NONE',  ( 0.000000000000000000, 14.87816164169115218, 4.342730381189920941 ) ) ;
#4302=DIRECTION ( 'NONE',  ( 0.000000000000000000, 0.000000000000000000, -1.000000000000000000 ) ) ;
#4305=CARTESIAN_POINT ( 'NONE',  ( 8.000000000000000000, -12.46108038583301436, -15.64357617739007722 ) ) ;
#4326=LINE ( 'NONE', #26281, #28940 ) ;
#4363=EDGE_CURVE ( 'NONE', #26963, #32273, #24953, .T. ) ;
#4371=AXIS2_PLACEMENT_3D ( 'NONE', #3331, #5492, #19669 ) ;
#4379=DIRECTION ( 'NONE',  ( -1.000000000000000000, 0.000000000000000000, 0.000000000000000000 ) ) ;
#4383=DIRECTION ( 'NONE',  ( 0.000000000000000000, 0.000000000000000000, -1.000000000000000000 ) ) ;
#4405=VERTEX_POINT ( 'NONE', #23306 ) ;
#4432=LINE ( 'NONE', #29444, #18787 ) ;
#4449=( NAMED_UNIT ( * ) PLANE_ANGLE_UNIT ( ) SI_UNIT ( $, .RADIAN. ) );
#4452=ORIENTED_EDGE ( 'NONE', *, *, #1176, .F. ) ;
#4456=VECTOR ( 'NONE', #24225, 1000.000000000000000 ) ;
#4463=AXIS2_PLACEMENT_3D ( 'NONE', #16099, #32498, #26948 ) ;
#4481=EDGE_CURVE ( 'NONE', #32097, #28443, #9447, .T. ) ;
#4483=CARTESIAN_POINT ( 'NONE',  ( 0.000000000000000000, 0.000000000000000000, 0.000000000000000000 ) ) ;
#4518=DIRECTION ( 'NONE',  ( -1.000000000000000000, 0.000000000000000000, 0.000000000000000000 ) ) ;
#4561=ORIENTED_EDGE ( 'NONE', *, *, #2926, .F. ) ;
#4579=VERTEX_POINT ( 'NONE', #35205 ) ;
#4586=ORIENTED_EDGE ( 'NONE', *, *, #11027, .T. ) ;
#4647=EDGE_CURVE ( 'NONE', #21593, #18755, #15721, .T. ) ;
#4715=CYLINDRICAL_SURFACE ( 'NONE', #23752, 7.199999999999994849 ) ;
#4739=ORIENTED_EDGE ( 'NONE', *, *, #20853, .T. ) ;
#4760=ORIENTED_EDGE ( 'NONE', *, *, #11760, .T. ) ;
#4768=VECTOR ( 'NONE', #29640, 1000.000000000000000 ) ;
#4802=EDGE_CURVE ( 'NONE', #2896, #1026, #27635, .T. ) ;
#4835=VERTEX_POINT ( 'NONE', #7995 ) ;
#4854=VERTEX_POINT ( 'NONE', #23771 ) ;
#4859=CARTESIAN_POINT ( 'NONE',  ( 0.000000000000000000, -1.693188892523641798, -15.40623615209873876 ) ) ;
#4867=LINE ( 'NONE', #26475, #21457 ) ;
#4882=ORIENTED_EDGE ( 'NONE', *, *, #15628, .F. ) ;
#4901=VECTOR ( 'NONE', #24351, 1000.000000000000000 ) ;
#4926=ORIENTED_EDGE ( 'NONE', *, *, #10455, .T. ) ;
#4935=CARTESIAN_POINT ( 'NONE',  ( 4.000000000000000000, -19.77827456857333743, -2.969824084036673639 ) ) ;
#4953=DIRECTION ( 'NONE',  ( 0.000000000000000000, 0.000000000000000000, 1.000000000000000000 ) ) ;
#4975=CYLINDRICAL_SURFACE ( 'NONE', #4463, 7.199999999999994849 ) ;
#4983=DIRECTION ( 'NONE',  ( -1.000000000000000000, 0.000000000000000000, 0.000000000000000000 ) ) ;
#5020=DIRECTION ( 'NONE',  ( 0.000000000000000000, -0.8660254037844433705, 0.4999999999999918954 ) ) ;
#5054=CYLINDRICAL_SURFACE ( 'NONE', #35202, 15.49899999999998457 ) ;
#5055=ORIENTED_EDGE ( 'NONE', *, *, #16264, .F. ) ;
#5060=ORIENTED_EDGE ( 'NONE', *, *, #2411, .F. ) ;
#5074=CARTESIAN_POINT ( 'NONE',  ( 4.000000000000000000, 0.5097555531873367851, 19.99350267651958291 ) ) ;
#5077=ORIENTED_EDGE ( 'NONE', *, *, #6885, .T. ) ;
#5093=FACE_OUTER_BOUND ( 'NONE', #24107, .T. ) ;
#5099=VECTOR ( 'NONE', #5822, 1000.000000000000000 ) ;
#5122=EDGE_CURVE ( 'NONE', #18755, #33477, #10451, .T. ) ;
#5123=DIRECTION ( 'NONE',  ( 1.000000000000000000, -0.000000000000000000, 0.000000000000000000 ) ) ;
#5131=CARTESIAN_POINT ( 'NONE',  ( 0.000000000000000000, 19.60123832284022782, -3.973846525876240765 ) ) ;
#5146=DIRECTION ( 'NONE',  ( -1.000000000000000000, 0.000000000000000000, 0.000000000000000000 ) ) ;
#5147=LINE ( 'NONE', #24580, #30329 ) ;
#5151=DIRECTION ( 'NONE',  ( 1.000000000000000000, -0.000000000000000000, -0.000000000000000000 ) ) ;
#5153=CYLINDRICAL_SURFACE ( 'NONE', #2178, 15.49899999999998457 ) ;
#5155=CARTESIAN_POINT ( 'NONE',  ( 4.000000000000000000, 13.24207120356965461, 14.98824707027445768 ) ) ;
#5158=VERTEX_POINT ( 'NONE', #1994 ) ;
#5160=DIRECTION ( 'NONE',  ( 0.000000000000000000, -0.6427876096865456912, 0.7660444431189726844 ) ) ;
#5167=ORIENTED_EDGE ( 'NONE', *, *, #33726, .T. ) ;
#5182=EDGE_CURVE ( 'NONE', #32593, #5158, #14054, .T. ) ;
#5189=CARTESIAN_POINT ( 'NONE',  ( 0.000000000000000000, 0.000000000000000000, 0.000000000000000000 ) ) ;
#5207=ORIENTED_EDGE ( 'NONE', *, *, #241, .F. ) ;
#5238=ORIENTED_EDGE ( 'NONE', *, *, #20458, .F. ) ;
#5245=AXIS2_PLACEMENT_3D ( 'NONE', #28406, #30931, #3749 ) ;
#5254=VECTOR ( 'NONE', #26166, 1000.000000000000000 ) ;
#5271=CARTESIAN_POINT ( 'NONE',  ( -10.00000000000000000, 0.000000000000000000, 0.000000000000000000 ) ) ;
#5295=PRESENTATION_STYLE_ASSIGNMENT (( #13222 ) ) ;
#5314=CARTESIAN_POINT ( 'NONE',  ( 4.000000000000000000, 7.317194182740413666, -18.61340026142641690 ) ) ;
#5318=LINE ( 'NONE', #19153, #16229 ) ;
#5333=DIRECTION ( 'NONE',  ( -1.000000000000000000, 0.000000000000000000, 0.000000000000000000 ) ) ;
#5344=ADVANCED_FACE ( 'NONE', ( #19425 ), #5750, .T. ) ;
#5351=CARTESIAN_POINT ( 'NONE',  ( -10.00000000000000000, 0.000000000000000000, 0.000000000000000000 ) ) ;
#5355=LINE ( 'NONE', #2841, #17417 ) ;
#5357=DIRECTION ( 'NONE',  ( -1.000000000000000000, 0.000000000000000000, 0.000000000000000000 ) ) ;
#5359=CARTESIAN_POINT ( 'NONE',  ( 8.000000000000000000, -17.06000345190446055, 10.43821259704015425 ) ) ;
#5366=VERTEX_POINT ( 'NONE', #34364 ) ;
#5375=AXIS2_PLACEMENT_3D ( 'NONE', #23582, #26111, #12608 ) ;
#5376=DIRECTION ( 'NONE',  ( -1.000000000000000000, 0.000000000000000000, 0.000000000000000000 ) ) ;
#5381=EDGE_CURVE ( 'NONE', #18606, #22707, #26732, .T. ) ;
#5398=CARTESIAN_POINT ( 'NONE',  ( 0.000000000000000000, 1.693188892523745936, 15.40623615209872632 ) ) ;
#5402=CARTESIAN_POINT ( 'NONE',  ( 0.000000000000000000, 12.49559743815781587, 9.169462670380626790 ) ) ;
#5412=DIRECTION ( 'NONE',  ( 0.000000000000000000, 0.000000000000000000, 1.000000000000000000 ) ) ;
#5420=CARTESIAN_POINT ( 'NONE',  ( 8.000000000000000000, 0.000000000000000000, 0.000000000000000000 ) ) ;
#5431=LINE ( 'NONE', #27746, #12168 ) ;
#5440=CYLINDRICAL_SURFACE ( 'NONE', #20469, 19.99999999999998579 ) ;
#5449=EDGE_LOOP ( 'NONE', ( #20171, #15087, #11966, #4760 ) ) ;
#5458=VERTEX_POINT ( 'NONE', #4128 ) ;
#5470=AXIS2_PLACEMENT_3D ( 'NONE', #25373, #17063, #19747 ) ;
#5474=AXIS2_PLACEMENT_3D ( 'NONE', #29955, #22008, #35546 ) ;
#5491=DIRECTION ( 'NONE',  ( 0.000000000000000000, 0.000000000000000000, 1.000000000000000000 ) ) ;
#5492=DIRECTION ( 'NONE',  ( 1.000000000000000000, -0.000000000000000000, 0.000000000000000000 ) ) ;
#5496=DIRECTION ( 'NONE',  ( -1.000000000000000000, 0.000000000000000000, 0.000000000000000000 ) ) ;
#5505=CARTESIAN_POINT ( 'NONE',  ( 0.000000000000000000, -6.359167119270331625, -18.96209359615098577 ) ) ;
#5508=VERTEX_POINT ( 'NONE', #26251 ) ;
#5514=DIRECTION ( 'NONE',  ( 0.000000000000000000, 0.000000000000000000, -1.000000000000000000 ) ) ;
#5530=DIRECTION ( 'NONE',  ( 0.000000000000000000, 0.6427876096865403621, -0.7660444431189771253 ) ) ;
#5539=DIRECTION ( 'NONE',  ( 1.000000000000000000, -0.000000000000000000, -0.000000000000000000 ) ) ;
#5554=EDGE_CURVE ( 'NONE', #16680, #26953, #34793, .T. ) ;
#5562=EDGE_CURVE ( 'NONE', #31717, #20111, #12749, .T. ) ;
#5571=DIRECTION ( 'NONE',  ( 1.000000000000000000, -0.000000000000000000, -0.000000000000000000 ) ) ;
#5577=CYLINDRICAL_SURFACE ( 'NONE', #9484, 15.49899999999998457 ) ;
#5578=CIRCLE ( 'NONE', #27455, 19.99999999999998579 ) ;
#5592=CARTESIAN_POINT ( 'NONE',  ( 0.000000000000000000, -14.80634052301628145, 8.177498406287162069 ) ) ;
#5603=EDGE_CURVE ( 'NONE', #13189, #34283, #17517, .T. ) ;
#5608=AXIS2_PLACEMENT_3D ( 'NONE', #8631, #32778, #19603 ) ;
#5612=VERTEX_POINT ( 'NONE', #10229 ) ;
#5622=CIRCLE ( 'NONE', #33778, 7.199999999999993072 ) ;
#5623=DIRECTION ( 'NONE',  ( 0.000000000000000000, -0.6427876096865295930, -0.7660444431189862291 ) ) ;
#5642=VERTEX_POINT ( 'NONE', #29493 ) ;
#5665=ORIENTED_EDGE ( 'NONE', *, *, #31919, .F. ) ;
#5669=CARTESIAN_POINT ( 'NONE',  ( 0.000000000000000000, 0.000000000000000000, 0.000000000000000000 ) ) ;
#5676=AXIS2_PLACEMENT_3D ( 'NONE', #12152, #25489, #11979 ) ;
#5700=DIRECTION ( 'NONE',  ( -1.000000000000000000, 0.000000000000000000, 0.000000000000000000 ) ) ;
#5704=DIRECTION ( 'NONE',  ( -1.000000000000000000, 0.000000000000000000, 0.000000000000000000 ) ) ;
#5705=CARTESIAN_POINT ( 'NONE',  ( 0.000000000000000000, -14.48509162075970202, 8.733917826871310908 ) ) ;
#5717=DIRECTION ( 'NONE',  ( -1.000000000000000000, 0.000000000000000000, 0.000000000000000000 ) ) ;
#5732=EDGE_LOOP ( 'NONE', ( #13217, #2590, #11522, #16609 ) ) ;
#5748=CIRCLE ( 'NONE', #30479, 7.199999999999992184 ) ;
#5750=CYLINDRICAL_SURFACE ( 'NONE', #16364, 15.49899999999998457 ) ;
#5762=CARTESIAN_POINT ( 'NONE',  ( 0.000000000000000000, 16.59870953437685515, -3.253005020243678214 ) ) ;
#5802=ORIENTED_EDGE ( 'NONE', *, *, #22179, .F. ) ;
#5822=DIRECTION ( 'NONE',  ( -0.000000000000000000, 1.000000000000000000, 0.000000000000000000 ) ) ;
#5838=EDGE_CURVE ( 'NONE', #5458, #4835, #2032, .T. ) ;
#5842=EDGE_CURVE ( 'NONE', #6291, #21409, #31338, .T. ) ;
#5851=CYLINDRICAL_SURFACE ( 'NONE', #2505, 19.99999999999998579 ) ;
#5859=ORIENTED_EDGE ( 'NONE', *, *, #18675, .T. ) ;
#5862=CARTESIAN_POINT ( 'NONE',  ( 8.000000000000000000, -12.49559743815772528, -9.169462670380713831 ) ) ;
#5869=DIRECTION ( 'NONE',  ( 1.000000000000000000, -0.000000000000000000, -0.000000000000000000 ) ) ;
#5889=ORIENTED_EDGE ( 'NONE', *, *, #24415, .T. ) ;
#5895=DIRECTION ( 'NONE',  ( -1.000000000000000000, 0.000000000000000000, 0.000000000000000000 ) ) ;
#5931=DIRECTION ( 'NONE',  ( 0.000000000000000000, 0.000000000000000000, -1.000000000000000000 ) ) ;
#5935=CIRCLE ( 'NONE', #19702, 19.99999999999998579 ) ;
#5945=ORIENTED_EDGE ( 'NONE', *, *, #26127, .T. ) ;
#5950=ORIENTED_EDGE ( 'NONE', *, *, #18733, .F. ) ;
#5955=CARTESIAN_POINT ( 'NONE',  ( 8.000000000000000000, -3.678165988948487009, -15.05623113391071044 ) ) ;
#5970=CARTESIAN_POINT ( 'NONE',  ( 8.000000000000000000, -13.24207120356975587, 14.98824707027438130 ) ) ;
#5975=CARTESIAN_POINT ( 'NONE',  ( 8.000000000000000000, 19.77827456857338007, -2.969824084036535528 ) ) ;
#5980=ADVANCED_FACE ( 'NONE', ( #9285 ), #28555, .T. ) ;
#5993=ORIENTED_EDGE ( 'NONE', *, *, #2408, .F. ) ;
#6011=EDGE_CURVE ( 'NONE', #4002, #26625, #10108, .T. ) ;
#6037=CIRCLE ( 'NONE', #33084, 7.200000000000000178 ) ;
#6073=VECTOR ( 'NONE', #22215, 1000.000000000000000 ) ;
#6074=DIRECTION ( 'NONE',  ( 0.000000000000000000, 0.000000000000000000, 1.000000000000000000 ) ) ;
#6101=AXIS2_PLACEMENT_3D ( 'NONE', #34463, #28871, #4223 ) ;
#6105=CIRCLE ( 'NONE', #3242, 7.199999999999992184 ) ;
#6107=LINE ( 'NONE', #33304, #16871 ) ;
#6110=DIRECTION ( 'NONE',  ( 0.000000000000000000, 0.000000000000000000, 1.000000000000000000 ) ) ;
#6117=ORIENTED_EDGE ( 'NONE', *, *, #878, .T. ) ;
#6152=ORIENTED_EDGE ( 'NONE', *, *, #13220, .T. ) ;
#6155=VECTOR ( 'NONE', #21324, 1000.000000000000000 ) ;
#6195=DIRECTION ( 'NONE',  ( -1.000000000000000000, 0.000000000000000000, 0.000000000000000000 ) ) ;
#6200=ORIENTED_EDGE ( 'NONE', *, *, #25729, .T. ) ;
#6210=EDGE_LOOP ( 'NONE', ( #13811, #34698, #5055, #32166 ) ) ;
#6242=EDGE_CURVE ( 'NONE', #10299, #7183, #31366, .T. ) ;
#6248=ORIENTED_EDGE ( 'NONE', *, *, #32571, .T. ) ;
#6260=DIRECTION ( 'NONE',  ( -1.000000000000000000, 0.000000000000000000, 0.000000000000000000 ) ) ;
#6277=CARTESIAN_POINT ( 'NONE',  ( 0.000000000000000000, 0.000000000000000000, 0.000000000000000000 ) ) ;
#6279=EDGE_CURVE ( 'NONE', #2211, #7746, #22738, .T. ) ;
#6281=VECTOR ( 'NONE', #13921, 1000.000000000000000 ) ;
#6290=ORIENTED_EDGE ( 'NONE', *, *, #2985, .F. ) ;
#6291=VERTEX_POINT ( 'NONE', #2814 ) ;
#6312=DIRECTION ( 'NONE',  ( -1.000000000000000000, 0.000000000000000000, 0.000000000000000000 ) ) ;
#6328=VECTOR ( 'NONE', #18358, 1000.000000000000000 ) ;
#6333=DIRECTION ( 'NONE',  ( -1.000000000000000000, 0.000000000000000000, 0.000000000000000000 ) ) ;
#6389=DIRECTION ( 'NONE',  ( -1.000000000000000000, 0.000000000000000000, 0.000000000000000000 ) ) ;
#6401=EDGE_CURVE ( 'NONE', #15022, #9129, #28508, .T. ) ;
#6405=EDGE_CURVE ( 'NONE', #9040, #12726, #2083, .T. ) ;
#6406=EDGE_CURVE ( 'NONE', #7746, #13301, #28332, .T. ) ;
#6456=LINE ( 'NONE', #33468, #28071 ) ;
#6464=VERTEX_POINT ( 'NONE', #9415 ) ;
#6502=DIRECTION ( 'NONE',  ( 0.000000000000000000, 0.000000000000000000, 1.000000000000000000 ) ) ;
#6510=EDGE_LOOP ( 'NONE', ( #14551, #19859, #15639, #28204, #10827, #22176 ) ) ;
#6533=VERTEX_POINT ( 'NONE', #22919 ) ;
#6567=CARTESIAN_POINT ( 'NONE',  ( 8.000000000000000000, 14.48509162075973755, -8.733917826871222090 ) ) ;
#6585=DIRECTION ( 'NONE',  ( 0.000000000000000000, -0.9848077530122063550, -0.1736481776669404342 ) ) ;
#6590=AXIS2_PLACEMENT_3D ( 'NONE', #11942, #3851, #4383 ) ;
#6595=ORIENTED_EDGE ( 'NONE', *, *, #35267, .T. ) ;
#6631=VECTOR ( 'NONE', #20373, 1000.000000000000000 ) ;
#6639=ORIENTED_EDGE ( 'NONE', *, *, #25303, .F. ) ;
#6662=ORIENTED_EDGE ( 'NONE', *, *, #30229, .F. ) ;
#6677=EDGE_LOOP ( 'NONE', ( #31133, #10041, #15314, #20296 ) ) ;
#6685=VERTEX_POINT ( 'NONE', #5970 ) ;
#6686=DIRECTION ( 'NONE',  ( 0.000000000000000000, 0.000000000000000000, 1.000000000000000000 ) ) ;
#6721=CIRCLE ( 'NONE', #11337, 7.199999999999998401 ) ;
#6727=FACE_OUTER_BOUND ( 'NONE', #914, .T. ) ;
#6735=ORIENTED_EDGE ( 'NONE', *, *, #11682, .F. ) ;
#6745=AXIS2_PLACEMENT_3D ( 'NONE', #33258, #14495, #28209 ) ;
#6754=CARTESIAN_POINT ( 'NONE',  ( 0.000000000000000000, -6.860320204751236162, 13.89802171851381551 ) ) ;
#6768=ORIENTED_EDGE ( 'NONE', *, *, #13286, .F. ) ;
#6772=FILL_AREA_STYLE ('',( #18098 ) ) ;
#6773=CARTESIAN_POINT ( 'NONE',  ( 0.000000000000000000, 0.000000000000000000, 0.000000000000000000 ) ) ;
#6786=CARTESIAN_POINT ( 'NONE',  ( 0.000000000000000000, 5.400000000000000355, 0.9999999999999985567 ) ) ;
#6798=DIRECTION ( 'NONE',  ( -1.000000000000000000, 0.000000000000000000, 0.000000000000000000 ) ) ;
#6801=DIRECTION ( 'NONE',  ( -1.000000000000000000, 0.000000000000000000, 0.000000000000000000 ) ) ;
#6818=ORIENTED_EDGE ( 'NONE', *, *, #4238, .F. ) ;
#6820=AXIS2_PLACEMENT_3D ( 'NONE', #1520, #2071, #7273 ) ;
#6871=ORIENTED_EDGE ( 'NONE', *, *, #13263, .T. ) ;
#6883=CARTESIAN_POINT ( 'NONE',  ( 8.000000000000000000, -14.48509162075970202, 8.733917826871310908 ) ) ;
#6885=EDGE_CURVE ( 'NONE', #31265, #6533, #8133, .T. ) ;
#6895=CARTESIAN_POINT ( 'NONE',  ( 4.000000000000000000, -17.06000345190446055, 10.43821259704015603 ) ) ;
#6909=CARTESIAN_POINT ( 'NONE',  ( 8.000000000000000000, 0.000000000000000000, 0.000000000000000000 ) ) ;
#6918=CARTESIAN_POINT ( 'NONE',  ( 8.000000000000000000, 12.46108038583314936, 15.64357617739001860 ) ) ;
#6920=AXIS2_PLACEMENT_3D ( 'NONE', #31117, #6801, #30937 ) ;
#6928=EDGE_CURVE ( 'NONE', #24111, #20033, #9197, .T. ) ;
#6938=DIRECTION ( 'NONE',  ( -1.000000000000000000, 0.000000000000000000, 0.000000000000000000 ) ) ;
#6949=CARTESIAN_POINT ( 'NONE',  ( 0.000000000000000000, -11.11653975335798528, 12.74840161668727134 ) ) ;
#6959=LINE ( 'NONE', #28933, #7570 ) ;
#6961=VERTEX_POINT ( 'NONE', #3461 ) ;
#6966=DIRECTION ( 'NONE',  ( 1.000000000000000000, -0.000000000000000000, 0.000000000000000000 ) ) ;
#6970=DIRECTION ( 'NONE',  ( -1.000000000000000000, 0.000000000000000000, 0.000000000000000000 ) ) ;
#6999=VERTEX_POINT ( 'NONE', #25599 ) ;
#7007=ADVANCED_FACE ( 'NONE', ( #22689 ), #3283, .T. ) ;
#7012=DIRECTION ( 'NONE',  ( -1.000000000000000000, 0.000000000000000000, 0.000000000000000000 ) ) ;
#7020=ORIENTED_EDGE ( 'NONE', *, *, #17193, .F. ) ;
#7040=LINE ( 'NONE', #23437, #10203 ) ;
#7050=AXIS2_PLACEMENT_3D ( 'NONE', #20137, #33013, #24560 ) ;
#7111=ORIENTED_EDGE ( 'NONE', *, *, #17035, .F. ) ;
#7113=DIRECTION ( 'NONE',  ( -1.000000000000000000, 0.000000000000000000, 0.000000000000000000 ) ) ;
#7115=CARTESIAN_POINT ( 'NONE',  ( 8.000000000000000000, -1.693188892523842082, 15.40623615209871566 ) ) ;
#7124=AXIS2_PLACEMENT_3D ( 'NONE', #5592, #11511, #30772 ) ;
#7138=ORIENTED_EDGE ( 'NONE', *, *, #9094, .T. ) ;
#7160=VERTEX_POINT ( 'NONE', #12624 ) ;
#7183=VERTEX_POINT ( 'NONE', #35613 ) ;
#7216=EDGE_LOOP ( 'NONE', ( #2726, #13340, #28095, #8363 ) ) ;
#7223=ORIENTED_EDGE ( 'NONE', *, *, #24381, .F. ) ;
#7226=AXIS2_PLACEMENT_3D ( 'NONE', #10899, #30341, #29985 ) ;
#7235=DIRECTION ( 'NONE',  ( 0.000000000000000000, -0.6427876096865456912, 0.7660444431189726844 ) ) ;
#7255=EDGE_LOOP ( 'NONE', ( #23658, #22124, #33272, #23675 ) ) ;
#7260=CARTESIAN_POINT ( 'NONE',  ( 4.000000000000000000, -12.46108038583301791, -15.64357617739007722 ) ) ;
#7267=AXIS2_PLACEMENT_3D ( 'NONE', #8389, #2318, #21721 ) ;
#7273=DIRECTION ( 'NONE',  ( 0.000000000000000000, 0.000000000000000000, 1.000000000000000000 ) ) ;
#7288=DIRECTION ( 'NONE',  ( -1.000000000000000000, 0.000000000000000000, 0.000000000000000000 ) ) ;
#7291=EDGE_CURVE ( 'NONE', #32647, #8637, #22428, .T. ) ;
#7299=ORIENTED_EDGE ( 'NONE', *, *, #35455, .F. ) ;
#7306=SURFACE_STYLE_FILL_AREA ( #6772 ) ;
#7308=LINE ( 'NONE', #1923, #30186 ) ;
#7323=EDGE_CURVE ( 'NONE', #11554, #16212, #11902, .T. ) ;
#7326=ORIENTED_EDGE ( 'NONE', *, *, #23562, .F. ) ;
#7338=DIRECTION ( 'NONE',  ( 0.000000000000000000, 0.3420201433256629953, 0.9396926207859104263 ) ) ;
#7358=CARTESIAN_POINT ( 'NONE',  ( 8.000000000000000000, 14.18878633068169925, -6.236773481717946765 ) ) ;
#7366=DIRECTION ( 'NONE',  ( 0.000000000000000000, 0.000000000000000000, 1.000000000000000000 ) ) ;
#7378=CYLINDRICAL_SURFACE ( 'NONE', #30521, 7.199999999999994849 ) ;
#7386=CARTESIAN_POINT ( 'NONE',  ( -10.00000000000000000, 0.000000000000000000, 0.000000000000000000 ) ) ;
#7394=ORIENTED_EDGE ( 'NONE', *, *, #28358, .F. ) ;
#7417=CIRCLE ( 'NONE', #15440, 7.199999999999990408 ) ;
#7423=FACE_OUTER_BOUND ( 'NONE', #35224, .T. ) ;
#7439=VECTOR ( 'NONE', #9763, 1000.000000000000000 ) ;
#7442=DIRECTION ( 'NONE',  ( -1.000000000000000000, 0.000000000000000000, 0.000000000000000000 ) ) ;
#7443=VERTEX_POINT ( 'NONE', #29798 ) ;
#7444=ORIENTED_EDGE ( 'NONE', *, *, #1176, .T. ) ;
#7446=AXIS2_PLACEMENT_3D ( 'NONE', #17286, #3633, #28955 ) ;
#7449=ORIENTED_EDGE ( 'NONE', *, *, #15260, .F. ) ;
#7459=EDGE_CURVE ( 'NONE', #31803, #32697, #14186, .T. ) ;
#7471=DIRECTION ( 'NONE',  ( 0.000000000000000000, 0.000000000000000000, 1.000000000000000000 ) ) ;
#7474=CARTESIAN_POINT ( 'NONE',  ( 8.000000000000000000, 11.11653975335807587, -12.74840161668719851 ) ) ;
#7488=ORIENTED_EDGE ( 'NONE', *, *, #22566, .F. ) ;
#7498=ORIENTED_EDGE ( 'NONE', *, *, #5562, .F. ) ;
#7510=CARTESIAN_POINT ( 'NONE',  ( 8.000000000000000000, 8.605879768205412006, -12.89022243466699535 ) ) ;
#7511=CIRCLE ( 'NONE', #29938, 7.199999999999986855 ) ;
#7514=LINE ( 'NONE', #18132, #13610 ) ;
#7521=LINE ( 'NONE', #26799, #12487 ) ;
#7526=PRODUCT ( 'spur gear_iso_ISO - Spur gear 2M 18T 20PA 8FW ---S18A75H50L8.0S1', 'spur gear_iso_ISO - Spur gear 2M 18T 20PA 8FW ---S18A75H50L8.0S1', '', ( #14508 ) ) ;
#7528=LINE ( 'NONE', #7358, #32445 ) ;
#7540=EDGE_CURVE ( 'NONE', #29334, #4579, #24004, .T. ) ;
#7541=DIRECTION ( 'NONE',  ( 0.000000000000000000, 0.000000000000000000, 1.000000000000000000 ) ) ;
#7543=ORIENTED_EDGE ( 'NONE', *, *, #34012, .T. ) ;
#7546=DIRECTION ( 'NONE',  ( 0.000000000000000000, 0.000000000000000000, 1.000000000000000000 ) ) ;
#7564=ORIENTED_EDGE ( 'NONE', *, *, #24730, .F. ) ;
#7570=VECTOR ( 'NONE', #13440, 1000.000000000000000 ) ;
#7572=DIRECTION ( 'NONE',  ( -1.000000000000000000, 0.000000000000000000, 0.000000000000000000 ) ) ;
#7596=FACE_OUTER_BOUND ( 'NONE', #14119, .T. ) ;
#7653=DIRECTION ( 'NONE',  ( -1.000000000000000000, 0.000000000000000000, 0.000000000000000000 ) ) ;
#7687=CARTESIAN_POINT ( 'NONE',  ( 0.000000000000000000, 1.693188892523948885, -15.40623615209870323 ) ) ;
#7691=ORIENTED_EDGE ( 'NONE', *, *, #10109, .F. ) ;
#7694=EDGE_LOOP ( 'NONE', ( #1040, #26091, #28918, #4176 ) ) ;
#7715=FACE_OUTER_BOUND ( 'NONE', #9130, .T. ) ;
#7717=DIRECTION ( 'NONE',  ( -1.000000000000000000, 0.000000000000000000, 0.000000000000000000 ) ) ;
#7721=CARTESIAN_POINT ( 'NONE',  ( 8.000000000000000000, -11.19999565274241782, -10.71350075272084545 ) ) ;
#7744=DIRECTION ( 'NONE',  ( 0.000000000000000000, -0.8660254037844329345, -0.5000000000000101030 ) ) ;
#7746=VERTEX_POINT ( 'NONE', #25450 ) ;
#7763=CARTESIAN_POINT ( 'NONE',  ( 8.000000000000000000, 15.46619997295642079, 1.007799283846740002 ) ) ;
#7771=CARTESIAN_POINT ( 'NONE',  ( 4.000000000000000000, -13.24207120356975587, 14.98824707027438485 ) ) ;
#7792=EDGE_CURVE ( 'NONE', #9366, #2211, #24593, .T. ) ;
#7813=CARTESIAN_POINT ( 'NONE',  ( 0.000000000000000000, -12.49559743815785140, 9.169462670380546854 ) ) ;
#7817=CIRCLE ( 'NONE', #905, 19.99999999999998579 ) ;
#7818=DIRECTION ( 'NONE',  ( 0.000000000000000000, 0.3420201433256693235, -0.9396926207859082059 ) ) ;
#7828=CARTESIAN_POINT ( 'NONE',  ( 0.000000000000000000, 14.80634052301623171, -8.177498406287266874 ) ) ;
#7832=DIRECTION ( 'NONE',  ( 0.000000000000000000, 0.000000000000000000, 1.000000000000000000 ) ) ;
#7849=CARTESIAN_POINT ( 'NONE',  ( 8.000000000000000000, 0.000000000000000000, 0.000000000000000000 ) ) ;
#7870=CARTESIAN_POINT ( 'NONE',  ( 0.000000000000000000, -16.71027810728550733, -2.620268201066114688 ) ) ;
#7873=VERTEX_POINT ( 'NONE', #18483 ) ;
#7887=ORIENTED_EDGE ( 'NONE', *, *, #5554, .T. ) ;
#7888=ORIENTED_EDGE ( 'NONE', *, *, #32019, .F. ) ;
#7950=FACE_OUTER_BOUND ( 'NONE', #22565, .T. ) ;
#7959=DIRECTION ( 'NONE',  ( 0.000000000000000000, 0.000000000000000000, 1.000000000000000000 ) ) ;
#7995=CARTESIAN_POINT ( 'NONE',  ( 0.000000000000000000, -12.46108038583323285, 15.64357617738992801 ) ) ;
#7996=EDGE_LOOP ( 'NONE', ( #33121, #30769, #32061, #33696 ) ) ;
#8001=DIRECTION ( 'NONE',  ( -1.000000000000000000, 0.000000000000000000, 0.000000000000000000 ) ) ;
#8003=ORIENTED_EDGE ( 'NONE', *, *, #14371, .F. ) ;
#8025=EDGE_CURVE ( 'NONE', #10671, #27661, #1581, .T. ) ;
#8033=CIRCLE ( 'NONE', #1151, 19.99999999999998579 ) ;
#8049=CARTESIAN_POINT ( 'NONE',  ( 8.000000000000000000, 16.71027810728552154, -2.620268201066000113 ) ) ;
#8053=VECTOR ( 'NONE', #24481, 1000.000000000000000 ) ;
#8057=VERTEX_POINT ( 'NONE', #27498 ) ;
#8091=ORIENTED_EDGE ( 'NONE', *, *, #12062, .T. ) ;
#8133=LINE ( 'NONE', #30110, #384 ) ;
#8160=CARTESIAN_POINT ( 'NONE',  ( 0.000000000000000000, 0.000000000000000000, 0.000000000000000000 ) ) ;
#8179=DIRECTION ( 'NONE',  ( 0.000000000000000000, 0.000000000000000000, 1.000000000000000000 ) ) ;
#8190=FACE_OUTER_BOUND ( 'NONE', #29567, .T. ) ;
#8207=CARTESIAN_POINT ( 'NONE',  ( 8.000000000000000000, -16.71027810728550733, 4.579731798933884157 ) ) ;
#8209=ADVANCED_FACE ( 'NONE', ( #25941 ), #12066, .T. ) ;
#8233=ORIENTED_EDGE ( 'NONE', *, *, #11682, .T. ) ;
#8235=CARTESIAN_POINT ( 'NONE',  ( 8.000000000000000000, 5.482169781018835231, 16.00140663693125376 ) ) ;
#8244=DIRECTION ( 'NONE',  ( 0.000000000000000000, -0.8660254037844432595, 0.4999999999999920619 ) ) ;
#8268=ORIENTED_EDGE ( 'NONE', *, *, #31688, .T. ) ;
#8285=DIRECTION ( 'NONE',  ( -1.000000000000000000, 0.000000000000000000, 0.000000000000000000 ) ) ;
#8305=EDGE_CURVE ( 'NONE', #19752, #16680, #31517, .T. ) ;
#8316=EDGE_CURVE ( 'NONE', #17379, #21593, #10159, .T. ) ;
#8331=DIRECTION ( 'NONE',  ( -1.000000000000000000, 0.000000000000000000, 0.000000000000000000 ) ) ;
#8336=DIRECTION ( 'NONE',  ( 0.000000000000000000, 0.9848077530122073542, 0.1736481776669338839 ) ) ;
#8363=ORIENTED_EDGE ( 'NONE', *, *, #13737, .F. ) ;
#8367=ORIENTED_EDGE ( 'NONE', *, *, #714, .F. ) ;
#8377=AXIS2_PLACEMENT_3D ( 'NONE', #31480, #34007, #28420 ) ;
#8389=CARTESIAN_POINT ( 'NONE',  ( 0.000000000000000000, 0.000000000000000000, 0.000000000000000000 ) ) ;
#8444=ORIENTED_EDGE ( 'NONE', *, *, #12646, .T. ) ;
#8458=DIRECTION ( 'NONE',  ( 0.000000000000000000, -0.9848077530122096857, 0.1736481776669208665 ) ) ;
#8462=VERTEX_POINT ( 'NONE', #7721 ) ;
#8470=AXIS2_PLACEMENT_3D ( 'NONE', #17303, #1119, #6686 ) ;
#8472=CARTESIAN_POINT ( 'NONE',  ( 8.000000000000000000, 0.000000000000000000, 0.000000000000000000 ) ) ;
#8490=CARTESIAN_POINT ( 'NONE',  ( -10.00000000000000000, 0.000000000000000000, 0.000000000000000000 ) ) ;
#8491=DIRECTION ( 'NONE',  ( -1.000000000000000000, 0.000000000000000000, 0.000000000000000000 ) ) ;
#8493=CIRCLE ( 'NONE', #32069, 7.199999999999986855 ) ;
#8502=AXIS2_PLACEMENT_3D ( 'NONE', #1, #10987, #21951 ) ;
#8514=DIRECTION ( 'NONE',  ( 0.000000000000000000, 0.000000000000000000, -1.000000000000000000 ) ) ;
#8534=DIRECTION ( 'NONE',  ( 0.000000000000000000, 0.000000000000000000, 1.000000000000000000 ) ) ;
#8544=DIRECTION ( 'NONE',  ( -1.000000000000000000, 0.000000000000000000, 0.000000000000000000 ) ) ;
#8547=ORIENTED_EDGE ( 'NONE', *, *, #17533, .T. ) ;
#8549=ORIENTED_EDGE ( 'NONE', *, *, #25774, .F. ) ;
#8590=ORIENTED_EDGE ( 'NONE', *, *, #6279, .F. ) ;
#8601=CARTESIAN_POINT ( 'NONE',  ( 8.000000000000000000, 3.872983346207417021, 0.9999999999999985567 ) ) ;
#8611=ORIENTED_EDGE ( 'NONE', *, *, #29961, .F. ) ;
#8618=DIRECTION ( 'NONE',  ( 0.000000000000000000, 0.000000000000000000, 1.000000000000000000 ) ) ;
#8622=CARTESIAN_POINT ( 'NONE',  ( 8.000000000000000000, 14.18878633068160866, 6.236773481718133283 ) ) ;
#8631=CARTESIAN_POINT ( 'NONE',  ( 0.000000000000000000, 0.000000000000000000, 0.000000000000000000 ) ) ;
#8637=VERTEX_POINT ( 'NONE', #10798 ) ;
#8653=FACE_OUTER_BOUND ( 'NONE', #25871, .T. ) ;
#8666=CIRCLE ( 'NONE', #34568, 7.199999999999998401 ) ;
#8690=VECTOR ( 'NONE', #12080, 1000.000000000000000 ) ;
#8707=CARTESIAN_POINT ( 'NONE',  ( -10.00000000000000000, 0.000000000000000000, 0.000000000000000000 ) ) ;
#8717=AXIS2_PLACEMENT_3D ( 'NONE', #28223, #28756, #28393 ) ;
#8728=DIRECTION ( 'NONE',  ( 0.000000000000000000, 0.000000000000000000, -1.000000000000000000 ) ) ;
#8754=CARTESIAN_POINT ( 'NONE',  ( 8.000000000000000000, 16.71027810728549667, 2.620268201066223934 ) ) ;
#8760=DIRECTION ( 'NONE',  ( -1.000000000000000000, 0.000000000000000000, 0.000000000000000000 ) ) ;
#8791=ORIENTED_EDGE ( 'NONE', *, *, #35444, .T. ) ;
#8799=CIRCLE ( 'NONE', #20874, 19.99999999999998579 ) ;
#8835=AXIS2_PLACEMENT_3D ( 'NONE', #23240, #34055, #23055 ) ;
#8841=EDGE_CURVE ( 'NONE', #7873, #32273, #856, .T. ) ;
#8852=EDGE_CURVE ( 'NONE', #31771, #8899, #14182, .T. ) ;
#8864=VECTOR ( 'NONE', #32758, 1000.000000000000000 ) ;
#8865=CARTESIAN_POINT ( 'NONE',  ( 0.000000000000000000, 8.605879768205412006, -12.89022243466699535 ) ) ;
#8888=CIRCLE ( 'NONE', #10631, 19.99999999999998579 ) ;
#8899=VERTEX_POINT ( 'NONE', #32002 ) ;
#8940=CYLINDRICAL_SURFACE ( 'NONE', #21908, 19.99999999999998579 ) ;
#8947=CIRCLE ( 'NONE', #12407, 19.99999999999998579 ) ;
#8959=CARTESIAN_POINT ( 'NONE',  ( 8.000000000000000000, 0.000000000000000000, 0.000000000000000000 ) ) ;
#8974=CARTESIAN_POINT ( 'NONE',  ( 8.000000000000000000, -12.49559743815785140, 9.169462670380546854 ) ) ;
#8978=CIRCLE ( 'NONE', #372, 7.199999999999993072 ) ;
#9006=DIRECTION ( 'NONE',  ( 0.000000000000000000, 0.000000000000000000, 1.000000000000000000 ) ) ;
#9022=CARTESIAN_POINT ( 'NONE',  ( 50.00005079999999680, 3.872983346207417021, -1.000000000000000000 ) ) ;
#9030=DIRECTION ( 'NONE',  ( 0.000000000000000000, 0.000000000000000000, 1.000000000000000000 ) ) ;
#9032=ORIENTED_EDGE ( 'NONE', *, *, #5838, .F. ) ;
#9040=VERTEX_POINT ( 'NONE', #10404 ) ;
#9051=PLANE ( 'NONE',  #13282 ) ;
#9063=AXIS2_PLACEMENT_3D ( 'NONE', #13860, #21775, #1688 ) ;
#9065=EDGE_CURVE ( 'NONE', #32703, #656, #5622, .T. ) ;
#9071=LINE ( 'NONE', #3867, #26201 ) ;
#9094=EDGE_CURVE ( 'NONE', #1605, #12650, #27673, .T. ) ;
#9107=AXIS2_PLACEMENT_3D ( 'NONE', #758, #19818, #14432 ) ;
#9108=DIRECTION ( 'NONE',  ( -1.000000000000000000, 0.000000000000000000, 0.000000000000000000 ) ) ;
#9111=CARTESIAN_POINT ( 'NONE',  ( 0.000000000000000000, 15.46619997295642079, 1.007799283846740002 ) ) ;
#9129=VERTEX_POINT ( 'NONE', #30022 ) ;
#9130=EDGE_LOOP ( 'NONE', ( #19481, #31487, #1424, #17241 ) ) ;
#9147=DIRECTION ( 'NONE',  ( -1.000000000000000000, 0.000000000000000000, 0.000000000000000000 ) ) ;
#9149=DIRECTION ( 'NONE',  ( 0.000000000000000000, 0.000000000000000000, 1.000000000000000000 ) ) ;
#9163=CARTESIAN_POINT ( 'NONE',  ( 0.000000000000000000, 10.62435788049443808, 13.16139124467922272 ) ) ;
#9172=APPLICATION_CONTEXT ( 'automotive_design' ) ;
#9197=LINE ( 'NONE', #33506, #29698 ) ;
#9232=UNCERTAINTY_MEASURE_WITH_UNIT (LENGTH_MEASURE( 1.000000000000000082E-05 ), #1733, 'distance_accuracy_value', 'NONE');
#9234=AXIS2_PLACEMENT_3D ( 'NONE', #18128, #29314, #32357 ) ;
#9238=CYLINDRICAL_SURFACE ( 'NONE', #35545, 7.199999999999993960 ) ;
#9285=FACE_OUTER_BOUND ( 'NONE', #33390, .T. ) ;
#9286=EDGE_CURVE ( 'NONE', #24979, #1452, #24000, .T. ) ;
#9287=CARTESIAN_POINT ( 'NONE',  ( 0.000000000000000000, 13.24207120356965461, 14.98824707027445768 ) ) ;
#9297=ORIENTED_EDGE ( 'NONE', *, *, #19670, .T. ) ;
#9299=DIRECTION ( 'NONE',  ( -1.000000000000000000, 0.000000000000000000, 0.000000000000000000 ) ) ;
#9300=ORIENTED_EDGE ( 'NONE', *, *, #1342, .T. ) ;
#9334=CARTESIAN_POINT ( 'NONE',  ( 0.000000000000000000, 14.18878633068169925, -6.236773481717946765 ) ) ;
#9337=ORIENTED_EDGE ( 'NONE', *, *, #27958, .F. ) ;
#9347=ORIENTED_EDGE ( 'NONE', *, *, #4363, .F. ) ;
#9366=VERTEX_POINT ( 'NONE', #7813 ) ;
#9390=CYLINDRICAL_SURFACE ( 'NONE', #8470, 19.99999999999998579 ) ;
#9415=CARTESIAN_POINT ( 'NONE',  ( 0.000000000000000000, 19.60123832284017453, 3.973846525876500113 ) ) ;
#9428=EDGE_LOOP ( 'NONE', ( #5950, #16029, #26626, #26547 ) ) ;
#9439=CARTESIAN_POINT ( 'NONE',  ( 8.000000000000000000, 16.59870953437680896, 10.45300502024389822 ) ) ;
#9444=DIRECTION ( 'NONE',  ( -1.000000000000000000, 0.000000000000000000, -0.000000000000000000 ) ) ;
#9447=LINE ( 'NONE', #12330, #12871 ) ;
#9448=ORIENTED_EDGE ( 'NONE', *, *, #25398, .T. ) ;
#9468=VERTEX_POINT ( 'NONE', #24217 ) ;
#9484=AXIS2_PLACEMENT_3D ( 'NONE', #27364, #3055, #33954 ) ;
#9498=LINE ( 'NONE', #31814, #34132 ) ;
#9542=DIRECTION ( 'NONE',  ( 0.000000000000000000, 0.000000000000000000, 1.000000000000000000 ) ) ;
#9550=DIRECTION ( 'NONE',  ( 0.000000000000000000, -0.9848077530122062440, -0.1736481776669401844 ) ) ;
#9587=AXIS2_PLACEMENT_3D ( 'NONE', #13456, #19025, #30024 ) ;
#9605=CIRCLE ( 'NONE', #32610, 15.49899999999997391 ) ;
#9608=DIRECTION ( 'NONE',  ( 0.000000000000000000, 0.9848077530122073542, 0.1736481776669339117 ) ) ;
#9612=CARTESIAN_POINT ( 'NONE',  ( 8.000000000000000000, 7.317194182740413666, -18.61340026142641690 ) ) ;
#9619=ORIENTED_EDGE ( 'NONE', *, *, #9065, .T. ) ;
#9623=FACE_OUTER_BOUND ( 'NONE', #9428, .T. ) ;
#9626=AXIS2_PLACEMENT_3D ( 'NONE', #31710, #6333, #14600 ) ;
#9634=DIRECTION ( 'NONE',  ( -1.000000000000000000, 0.000000000000000000, 0.000000000000000000 ) ) ;
#9646=FACE_OUTER_BOUND ( 'NONE', #20538, .T. ) ;
#9665=ADVANCED_FACE ( 'NONE', ( #33906 ), #9238, .T. ) ;
#9697=EDGE_LOOP ( 'NONE', ( #21078, #32258, #25799, #17429 ) ) ;
#9725=ORIENTED_EDGE ( 'NONE', *, *, #26389, .T. ) ;
#9749=FACE_OUTER_BOUND ( 'NONE', #30910, .T. ) ;
#9750=CIRCLE ( 'NONE', #16624, 19.99999999999998579 ) ;
#9758=CARTESIAN_POINT ( 'NONE',  ( 8.000000000000000000, 3.678165988948591814, 15.05623113391068379 ) ) ;
#9763=DIRECTION ( 'NONE',  ( -1.000000000000000000, 0.000000000000000000, 0.000000000000000000 ) ) ;
#9799=CIRCLE ( 'NONE', #13269, 7.199999999999998401 ) ;
#9802=AXIS2_PLACEMENT_3D ( 'NONE', #10716, #32859, #14107 ) ;
#9811=FACE_OUTER_BOUND ( 'NONE', #20165, .T. ) ;
#9822=DIRECTION ( 'NONE',  ( -1.000000000000000000, 0.000000000000000000, 0.000000000000000000 ) ) ;
#9830=AXIS2_PLACEMENT_3D ( 'NONE', #35349, #27245, #16048 ) ;
#9848=AXIS2_PLACEMENT_3D ( 'NONE', #3405, #33448, #31107 ) ;
#9857=EDGE_CURVE ( 'NONE', #6685, #876, #21277, .T. ) ;
#9858=CARTESIAN_POINT ( 'NONE',  ( 0.000000000000000000, -12.49559743815772350, -9.169462670380712055 ) ) ;
#9873=DIRECTION ( 'NONE',  ( -1.000000000000000000, 0.000000000000000000, 0.000000000000000000 ) ) ;
#9911=EDGE_LOOP ( 'NONE', ( #1332, #23959, #4586, #13788 ) ) ;
#9914=CARTESIAN_POINT ( 'NONE',  ( 8.000000000000000000, 13.24207120356986422, -14.98824707027427650 ) ) ;
#9915=ADVANCED_FACE ( 'NONE', ( #21451 ), #32806, .T. ) ;
#9929=AXIS2_PLACEMENT_3D ( 'NONE', #23643, #32100, #23089 ) ;
#9938=CARTESIAN_POINT ( 'NONE',  ( 0.000000000000000000, 0.000000000000000000, 0.000000000000000000 ) ) ;
#9995=ORIENTED_EDGE ( 'NONE', *, *, #24145, .F. ) ;
#10000=ORIENTED_EDGE ( 'NONE', *, *, #11236, .T. ) ;
#10007=PRESENTATION_STYLE_ASSIGNMENT (( #20614 ) ) ;
#10016=CARTESIAN_POINT ( 'NONE',  ( 8.000000000000000000, -19.60123832284022072, 3.973846525876368219 ) ) ;
#10021=ORIENTED_EDGE ( 'NONE', *, *, #20988, .F. ) ;
#10029=FACE_OUTER_BOUND ( 'NONE', #33976, .T. ) ;
#10038=DIRECTION ( 'NONE',  ( 1.000000000000000000, -0.000000000000000000, 0.000000000000000000 ) ) ;
#10040=CARTESIAN_POINT ( 'NONE',  ( 8.000000000000000000, 17.06000345190438594, 10.43821259704026794 ) ) ;
#10041=ORIENTED_EDGE ( 'NONE', *, *, #11042, .F. ) ;
#10052=AXIS2_PLACEMENT_3D ( 'NONE', #14681, #25695, #6585 ) ;
#10069=LINE ( 'NONE', #1982, #16124 ) ;
#10084=VERTEX_POINT ( 'NONE', #16925 ) ;
#10086=ORIENTED_EDGE ( 'NONE', *, *, #28853, .F. ) ;
#10099=VERTEX_POINT ( 'NONE', #17107 ) ;
#10108=CIRCLE ( 'NONE', #25042, 3.999999999999996447 ) ;
#10109=EDGE_CURVE ( 'NONE', #10620, #32703, #30459, .T. ) ;
#10118=ADVANCED_FACE ( 'NONE', ( #22162 ), #14582, .T. ) ;
#10126=ORIENTED_EDGE ( 'NONE', *, *, #24273, .T. ) ;
#10137=AXIS2_PLACEMENT_3D ( 'NONE', #18579, #29754, #26884 ) ;
#10150=LINE ( 'NONE', #1211, #25025 ) ;
#10159=CIRCLE ( 'NONE', #18760, 19.99999999999998579 ) ;
#10160=AXIS2_PLACEMENT_3D ( 'NONE', #14241, #14944, #4001 ) ;
#10163=EDGE_CURVE ( 'NONE', #5508, #16891, #29300, .T. ) ;
#10167=CARTESIAN_POINT ( 'NONE',  ( 0.000000000000000000, 3.678165988948591814, 15.05623113391068379 ) ) ;
#10168=AXIS2_PLACEMENT_3D ( 'NONE', #25831, #12128, #1504 ) ;
#10178=AXIS2_PLACEMENT_3D ( 'NONE', #20777, #7113, #7471 ) ;
#10203=VECTOR ( 'NONE', #14957, 1000.000000000000000 ) ;
#10205=CIRCLE ( 'NONE', #16508, 15.49899999999998279 ) ;
#10207=( GEOMETRIC_REPRESENTATION_CONTEXT ( 3 ) GLOBAL_UNCERTAINTY_ASSIGNED_CONTEXT ( ( #9232 ) ) GLOBAL_UNIT_ASSIGNED_CONTEXT ( ( #1733, #4449, #12718 ) ) REPRESENTATION_CONTEXT ( 'NONE', 'WORKASPACE' ) );
#10218=CYLINDRICAL_SURFACE ( 'NONE', #12109, 7.199999999999994849 ) ;
#10229=CARTESIAN_POINT ( 'NONE',  ( 8.000000000000000000, 0.5097555531873367851, 19.99350267651958291 ) ) ;
#10235=DIRECTION ( 'NONE',  ( -1.000000000000000000, 0.000000000000000000, 0.000000000000000000 ) ) ;
#10249=CIRCLE ( 'NONE', #17709, 19.99999999999998579 ) ;
#10251=CIRCLE ( 'NONE', #30375, 7.199999999999990408 ) ;
#10257=AXIS2_PLACEMENT_3D ( 'NONE', #19303, #19489, #8514 ) ;
#10258=CYLINDRICAL_SURFACE ( 'NONE', #148, 7.199999999999993960 ) ;
#10260=EDGE_LOOP ( 'NONE', ( #32478, #15, #29778, #2444 ) ) ;
#10267=DIRECTION ( 'NONE',  ( 0.000000000000000000, 0.000000000000000000, 1.000000000000000000 ) ) ;
#10278=CIRCLE ( 'NONE', #35014, 15.49899999999999700 ) ;
#10299=VERTEX_POINT ( 'NONE', #13292 ) ;
#10318=ORIENTED_EDGE ( 'NONE', *, *, #13006, .F. ) ;
#10345=CARTESIAN_POINT ( 'NONE',  ( 0.000000000000000000, 0.000000000000000000, 0.000000000000000000 ) ) ;
#10347=DIRECTION ( 'NONE',  ( 0.000000000000000000, 0.000000000000000000, 1.000000000000000000 ) ) ;
#10349=ADVANCED_FACE ( 'NONE', ( #32898 ), #13460, .T. ) ;
#10352=CARTESIAN_POINT ( 'NONE',  ( 8.000000000000000000, 0.3212489022565391261, 16.91141623315867193 ) ) ;
#10365=CARTESIAN_POINT ( 'NONE',  ( 8.000000000000000000, 0.000000000000000000, 0.000000000000000000 ) ) ;
#10369=CARTESIAN_POINT ( 'NONE',  ( 0.000000000000000000, 19.77827456857338007, 2.969824084036534639 ) ) ;
#10371=CARTESIAN_POINT ( 'NONE',  ( 8.000000000000000000, 0.000000000000000000, 0.000000000000000000 ) ) ;
#10372=ORIENTED_EDGE ( 'NONE', *, *, #28849, .T. ) ;
#10373=ORIENTED_EDGE ( 'NONE', *, *, #18675, .F. ) ;
#10377=VERTEX_POINT ( 'NONE', #9111 ) ;
#10378=VECTOR ( 'NONE', #24564, 1000.000000000000000 ) ;
#10399=AXIS2_PLACEMENT_3D ( 'NONE', #674, #28065, #31282 ) ;
#10404=CARTESIAN_POINT ( 'NONE',  ( 0.000000000000000000, 0.000000000000000000, 4.000000000000000000 ) ) ;
#10405=DIRECTION ( 'NONE',  ( -1.000000000000000000, 0.000000000000000000, 0.000000000000000000 ) ) ;
#10417=DIRECTION ( 'NONE',  ( -1.000000000000000000, 0.000000000000000000, 0.000000000000000000 ) ) ;
#10434=CIRCLE ( 'NONE', #31700, 7.199999999999994849 ) ;
#10448=DIRECTION ( 'NONE',  ( -1.000000000000000000, 0.000000000000000000, 0.000000000000000000 ) ) ;
#10451=LINE ( 'NONE', #27195, #8864 ) ;
#10452=ORIENTED_EDGE ( 'NONE', *, *, #14711, .F. ) ;
#10455=EDGE_CURVE ( 'NONE', #32273, #18735, #8033, .T. ) ;
#10460=ORIENTED_EDGE ( 'NONE', *, *, #7323, .F. ) ;
#10472=ORIENTED_EDGE ( 'NONE', *, *, #32076, .F. ) ;
#10480=CARTESIAN_POINT ( 'NONE',  ( 8.000000000000000000, 14.48509162075973755, -8.733917826871222090 ) ) ;
#10485=LINE ( 'NONE', #18400, #31413 ) ;
#10489=CARTESIAN_POINT ( 'NONE',  ( 0.000000000000000000, 11.19999565274250308, 10.71350075272077973 ) ) ;
#10509=ORIENTED_EDGE ( 'NONE', *, *, #27735, .F. ) ;
#10520=CARTESIAN_POINT ( 'NONE',  ( 8.000000000000000000, 0.000000000000000000, 0.000000000000000000 ) ) ;
#10522=VECTOR ( 'NONE', #549, 1000.000000000000000 ) ;
#10529=LINE ( 'NONE', #21318, #17949 ) ;
#10531=DIRECTION ( 'NONE',  ( -1.000000000000000000, 0.000000000000000000, 0.000000000000000000 ) ) ;
#10535=CARTESIAN_POINT ( 'NONE',  ( 8.000000000000000000, -11.19999565274241782, -10.71350075272084545 ) ) ;
#10538=DIRECTION ( 'NONE',  ( 0.000000000000000000, 0.000000000000000000, -1.000000000000000000 ) ) ;
#10541=EDGE_LOOP ( 'NONE', ( #28505, #11020, #21032, #10854 ) ) ;
#10549=EDGE_LOOP ( 'NONE', ( #1973, #13835, #20372, #16403 ) ) ;
#10551=VERTEX_POINT ( 'NONE', #24060 ) ;
#10578=AXIS2_PLACEMENT_3D ( 'NONE', #10352, #18620, #18076 ) ;
#10586=ORIENTED_EDGE ( 'NONE', *, *, #12569, .T. ) ;
#10604=CARTESIAN_POINT ( 'NONE',  ( 0.000000000000000000, 0.000000000000000000, 0.000000000000000000 ) ) ;
#10605=ADVANCED_FACE ( 'NONE', ( #9646 ), #26394, .T. ) ;
#10620=VERTEX_POINT ( 'NONE', #29450 ) ;
#10631=AXIS2_PLACEMENT_3D ( 'NONE', #6773, #9299, #17745 ) ;
#10645=DIRECTION ( 'NONE',  ( 1.000000000000000000, -0.000000000000000000, 0.000000000000000000 ) ) ;
#10653=EDGE_CURVE ( 'NONE', #19119, #19752, #21286, .T. ) ;
#10663=CARTESIAN_POINT ( 'NONE',  ( 8.000000000000000000, -11.11653975335780942, -12.74840161668743299 ) ) ;
#10671=VERTEX_POINT ( 'NONE', #18089 ) ;
#10680=ADVANCED_FACE ( 'NONE', ( #27816 ), #16092, .T. ) ;
#10687=( LENGTH_UNIT ( ) NAMED_UNIT ( * ) SI_UNIT ( .MILLI., .METRE. ) );
#10688=CARTESIAN_POINT ( 'NONE',  ( 0.000000000000000000, 14.48509162075973755, -8.733917826871222090 ) ) ;
#10694=FACE_OUTER_BOUND ( 'NONE', #27124, .T. ) ;
#10700=CARTESIAN_POINT ( 'NONE',  ( 8.000000000000000000, -10.62435788049451624, 13.16139124467916588 ) ) ;
#10709=CIRCLE ( 'NONE', #6101, 15.49900000000001121 ) ;
#10710=DIRECTION ( 'NONE',  ( -1.000000000000000000, 0.000000000000000000, 0.000000000000000000 ) ) ;
#10713=CARTESIAN_POINT ( 'NONE',  ( 0.000000000000000000, 0.000000000000000000, 0.000000000000000000 ) ) ;
#10716=CARTESIAN_POINT ( 'NONE',  ( -10.00000000000000000, 0.000000000000000000, 0.000000000000000000 ) ) ;
#10720=VECTOR ( 'NONE', #9108, 1000.000000000000000 ) ;
#10725=DIRECTION ( 'NONE',  ( -1.000000000000000000, 0.000000000000000000, 0.000000000000000000 ) ) ;
#10755=DIRECTION ( 'NONE',  ( 0.000000000000000000, 0.000000000000000000, -1.000000000000000000 ) ) ;
#10758=DIRECTION ( 'NONE',  ( 0.000000000000000000, 0.000000000000000000, 1.000000000000000000 ) ) ;
#10759=ORIENTED_EDGE ( 'NONE', *, *, #13704, .T. ) ;
#10761=FACE_OUTER_BOUND ( 'NONE', #13733, .T. ) ;
#10773=AXIS2_PLACEMENT_3D ( 'NONE', #24220, #24756, #32483 ) ;
#10783=VERTEX_POINT ( 'NONE', #11075 ) ;
#10789=LINE ( 'NONE', #29348, #12058 ) ;
#10798=CARTESIAN_POINT ( 'NONE',  ( 8.000000000000000000, -7.317194182740013098, -18.61340026142654480 ) ) ;
#10800=ADVANCED_FACE ( 'NONE', ( #13420 ), #13944, .T. ) ;
#10823=AXIS2_PLACEMENT_3D ( 'NONE', #2865, #5895, #33433 ) ;
#10827=ORIENTED_EDGE ( 'NONE', *, *, #35179, .F. ) ;
#10833=EDGE_LOOP ( 'NONE', ( #33185, #23415, #1996, #18028 ) ) ;
#10846=DIRECTION ( 'NONE',  ( -1.000000000000000000, 0.000000000000000000, 0.000000000000000000 ) ) ;
#10854=ORIENTED_EDGE ( 'NONE', *, *, #6401, .T. ) ;
#10870=CIRCLE ( 'NONE', #11990, 19.99999999999998579 ) ;
#10874=ORIENTED_EDGE ( 'NONE', *, *, #20988, .T. ) ;
#10899=CARTESIAN_POINT ( 'NONE',  ( 8.000000000000000000, 0.000000000000000000, 0.000000000000000000 ) ) ;
#10908=CARTESIAN_POINT ( 'NONE',  ( -10.00000000000000000, 0.000000000000000000, 0.000000000000000000 ) ) ;
#10915=VERTEX_POINT ( 'NONE', #23095 ) ;
#10917=CARTESIAN_POINT ( 'NONE',  ( 8.000000000000000000, -5.482169781018729537, -16.00140663693126086 ) ) ;
#10927=CARTESIAN_POINT ( 'NONE',  ( 0.000000000000000000, 0.000000000000000000, 0.000000000000000000 ) ) ;
#10929=EDGE_CURVE ( 'NONE', #24948, #6464, #27068, .T. ) ;
#10930=DIRECTION ( 'NONE',  ( 0.000000000000000000, -0.9848077530122062440, -0.1736481776669401844 ) ) ;
#10936=FACE_OUTER_BOUND ( 'NONE', #10549, .T. ) ;
#10943=DIRECTION ( 'NONE',  ( -1.000000000000000000, 0.000000000000000000, 0.000000000000000000 ) ) ;
#10957=ORIENTED_EDGE ( 'NONE', *, *, #27618, .F. ) ;
#10985=ORIENTED_EDGE ( 'NONE', *, *, #22566, .T. ) ;
#10987=DIRECTION ( 'NONE',  ( -1.000000000000000000, 0.000000000000000000, 0.000000000000000000 ) ) ;
#11001=ORIENTED_EDGE ( 'NONE', *, *, #35459, .T. ) ;
#11019=ORIENTED_EDGE ( 'NONE', *, *, #20246, .T. ) ;
#11020=ORIENTED_EDGE ( 'NONE', *, *, #17533, .F. ) ;
#11024=CARTESIAN_POINT ( 'NONE',  ( -10.00000000000000000, 0.000000000000000000, 0.000000000000000000 ) ) ;
#11026=FACE_OUTER_BOUND ( 'NONE', #24713, .T. ) ;
#11027=EDGE_CURVE ( 'NONE', #16212, #32593, #14823, .T. ) ;
#11042=EDGE_CURVE ( 'NONE', #12726, #4002, #12302, .T. ) ;
#11048=EDGE_CURVE ( 'NONE', #10551, #876, #30528, .T. ) ;
#11055=DIRECTION ( 'NONE',  ( 0.000000000000000000, -6.987080667128811173E-15, 1.000000000000000000 ) ) ;
#11059=DIRECTION ( 'NONE',  ( -1.000000000000000000, 0.000000000000000000, 0.000000000000000000 ) ) ;
#11075=CARTESIAN_POINT ( 'NONE',  ( 8.000000000000000000, 14.18878633068160866, 6.236773481718133283 ) ) ;
#11086=EDGE_LOOP ( 'NONE', ( #32418, #2466, #31523, #10874 ) ) ;
#11097=AXIS2_PLACEMENT_3D ( 'NONE', #28637, #7012, #9542 ) ;
#11100=AXIS2_PLACEMENT_3D ( 'NONE', #23881, #10725, #34869 ) ;
#11109=CIRCLE ( 'NONE', #12862, 15.49899999999998279 ) ;
#11132=ORIENTED_EDGE ( 'NONE', *, *, #11048, .F. ) ;
#11135=AXIS2_PLACEMENT_3D ( 'NONE', #10700, #2613, #8336 ) ;
#11141=AXIS2_PLACEMENT_3D ( 'NONE', #20693, #28997, #23049 ) ;
#11150=DIRECTION ( 'NONE',  ( -1.000000000000000000, 0.000000000000000000, 0.000000000000000000 ) ) ;
#11153=CARTESIAN_POINT ( 'NONE',  ( 8.000000000000000000, 1.693188892523948885, -15.40623615209870323 ) ) ;
#11156=CARTESIAN_POINT ( 'NONE',  ( 8.000000000000000000, 16.71027810728552154, -2.620268201066000113 ) ) ;
#11161=ORIENTED_EDGE ( 'NONE', *, *, #400, .F. ) ;
#11220=AXIS2_PLACEMENT_3D ( 'NONE', #34910, #10235, #13126 ) ;
#11228=CIRCLE ( 'NONE', #31352, 15.49899999999998279 ) ;
#11236=EDGE_CURVE ( 'NONE', #20895, #6291, #8666, .T. ) ;
#11241=FACE_OUTER_BOUND ( 'NONE', #30176, .T. ) ;
#11247=ADVANCED_FACE ( 'NONE', ( #2242 ), #32815, .T. ) ;
#11250=ORIENTED_EDGE ( 'NONE', *, *, #17528, .F. ) ;
#11251=EDGE_CURVE ( 'NONE', #192, #31803, #31092, .T. ) ;
#11256=ORIENTED_EDGE ( 'NONE', *, *, #9857, .F. ) ;
#11257=ORIENTED_EDGE ( 'NONE', *, *, #28839, .F. ) ;
#11264=CARTESIAN_POINT ( 'NONE',  ( 8.000000000000000000, 11.11653975335790179, 12.74840161668735661 ) ) ;
#11268=AXIS2_PLACEMENT_3D ( 'NONE', #25012, #335, #16354 ) ;
#11270=CARTESIAN_POINT ( 'NONE',  ( 8.000000000000000000, -14.18878633068163708, 6.236773481718040024 ) ) ;
#11283=CARTESIAN_POINT ( 'NONE',  ( 8.000000000000000000, -14.48509162075955281, -8.733917826871511636 ) ) ;
#11304=CYLINDRICAL_SURFACE ( 'NONE', #11381, 7.199999999999993960 ) ;
#11307=CARTESIAN_POINT ( 'NONE',  ( -10.00000000000000000, 0.000000000000000000, 0.000000000000000000 ) ) ;
#11329=DIRECTION ( 'NONE',  ( 0.000000000000000000, 0.000000000000000000, 1.000000000000000000 ) ) ;
#11337=AXIS2_PLACEMENT_3D ( 'NONE', #26504, #7572, #7744 ) ;
#11349=ORIENTED_EDGE ( 'NONE', *, *, #20539, .T. ) ;
#11373=VERTEX_POINT ( 'NONE', #30990 ) ;
#11374=ORIENTED_EDGE ( 'NONE', *, *, #3107, .F. ) ;
#11377=CARTESIAN_POINT ( 'NONE',  ( 8.000000000000000000, 15.46619997295644389, -1.007799283846741556 ) ) ;
#11381=AXIS2_PLACEMENT_3D ( 'NONE', #22273, #35447, #33267 ) ;
#11387=EDGE_CURVE ( 'NONE', #984, #11433, #10434, .T. ) ;
#11394=VERTEX_POINT ( 'NONE', #3287 ) ;
#11400=DIRECTION ( 'NONE',  ( -1.000000000000000000, 0.000000000000000000, 0.000000000000000000 ) ) ;
#11411=EDGE_CURVE ( 'NONE', #34524, #10671, #25786, .T. ) ;
#11433=VERTEX_POINT ( 'NONE', #5975 ) ;
#11469=AXIS2_PLACEMENT_3D ( 'NONE', #7849, #18837, #15949 ) ;
#11475=CARTESIAN_POINT ( 'NONE',  ( 50.00005079999999680, 0.000000000000000000, 0.000000000000000000 ) ) ;
#11476=ORIENTED_EDGE ( 'NONE', *, *, #21190, .F. ) ;
#11497=DIRECTION ( 'NONE',  ( -1.000000000000000000, 0.000000000000000000, 0.000000000000000000 ) ) ;
#11499=VERTEX_POINT ( 'NONE', #33874 ) ;
#11500=CYLINDRICAL_SURFACE ( 'NONE', #11268, 7.199999999999993960 ) ;
#11511=DIRECTION ( 'NONE',  ( -1.000000000000000000, 0.000000000000000000, 0.000000000000000000 ) ) ;
#11517=DIRECTION ( 'NONE',  ( -1.000000000000000000, 0.000000000000000000, 0.000000000000000000 ) ) ;
#11522=ORIENTED_EDGE ( 'NONE', *, *, #7291, .F. ) ;
#11541=CARTESIAN_POINT ( 'NONE',  ( 8.000000000000000000, 0.000000000000000000, 0.000000000000000000 ) ) ;
#11548=ORIENTED_EDGE ( 'NONE', *, *, #13070, .F. ) ;
#11552=DIRECTION ( 'NONE',  ( 0.000000000000000000, 0.000000000000000000, -1.000000000000000000 ) ) ;
#11554=VERTEX_POINT ( 'NONE', #15480 ) ;
#11573=CARTESIAN_POINT ( 'NONE',  ( 8.000000000000000000, 8.605879768205236147, 12.89022243466711615 ) ) ;
#11596=CYLINDRICAL_SURFACE ( 'NONE', #26056, 7.199999999999994849 ) ;
#11628=CARTESIAN_POINT ( 'NONE',  ( 8.000000000000000000, 16.59870953437680896, 3.253005020243904255 ) ) ;
#11650=CARTESIAN_POINT ( 'NONE',  ( 8.000000000000000000, -1.693188892523641798, -15.40623615209873876 ) ) ;
#11656=AXIS2_PLACEMENT_3D ( 'NONE', #4248, #9444, #23673 ) ;
#11664=CYLINDRICAL_SURFACE ( 'NONE', #24500, 15.49899999999998457 ) ;
#11667=ORIENTED_EDGE ( 'NONE', *, *, #26633, .F. ) ;
#11682=EDGE_CURVE ( 'NONE', #4062, #21331, #23665, .T. ) ;
#11695=CIRCLE ( 'NONE', #18018, 15.49899999999998457 ) ;
#11701=CARTESIAN_POINT ( 'NONE',  ( 8.000000000000000000, 14.87816164169121080, -4.342730381189718436 ) ) ;
#11707=DIRECTION ( 'NONE',  ( -1.000000000000000000, 0.000000000000000000, 0.000000000000000000 ) ) ;
#11745=FACE_OUTER_BOUND ( 'NONE', #21450, .T. ) ;
#11748=CIRCLE ( 'NONE', #34857, 15.49900000000001121 ) ;
#11760=EDGE_CURVE ( 'NONE', #13855, #22477, #25956, .T. ) ;
#11767=VECTOR ( 'NONE', #12352, 1000.000000000000000 ) ;
#11771=LINE ( 'NONE', #7260, #34120 ) ;
#11784=CARTESIAN_POINT ( 'NONE',  ( 8.000000000000000000, 6.359167119270718871, -18.96209359615085788 ) ) ;
#11807=EDGE_LOOP ( 'NONE', ( #33164, #4284, #31391, #32209 ) ) ;
#11846=CYLINDRICAL_SURFACE ( 'NONE', #25669, 7.199999999999993960 ) ;
#11849=AXIS2_PLACEMENT_3D ( 'NONE', #16918, #19275, #5623 ) ;
#11853=ORIENTED_EDGE ( 'NONE', *, *, #25078, .F. ) ;
#11863=SHAPE_REPRESENTATION ( 'spur gear_iso_ISO - Spur gear 2M 18T 20PA 8FW ---S18A75H50L8.0S1', ( #21307 ), #1229 ) ;
#11882=FACE_OUTER_BOUND ( 'NONE', #15038, .T. ) ;
#11902=CIRCLE ( 'NONE', #14773, 7.199999999999993960 ) ;
#11920=DIRECTION ( 'NONE',  ( 0.000000000000000000, 0.000000000000000000, 1.000000000000000000 ) ) ;
#11940=CARTESIAN_POINT ( 'NONE',  ( 8.000000000000000000, 7.317194182740155206, 18.61340026142653770 ) ) ;
#11942=CARTESIAN_POINT ( 'NONE',  ( 0.000000000000000000, -0.3212489022564151142, -16.91141623315864706 ) ) ;
#11966=ORIENTED_EDGE ( 'NONE', *, *, #25520, .F. ) ;
#11979=DIRECTION ( 'NONE',  ( 0.000000000000000000, -6.983129352544641692E-15, 1.000000000000000000 ) ) ;
#11984=VERTEX_POINT ( 'NONE', #9758 ) ;
#11990=AXIS2_PLACEMENT_3D ( 'NONE', #19269, #13535, #35511 ) ;
#12021=CARTESIAN_POINT ( 'NONE',  ( 8.000000000000000000, -0.3212489022566501484, 16.91141623315869680 ) ) ;
#12028=DIRECTION ( 'NONE',  ( -1.000000000000000000, 0.000000000000000000, 0.000000000000000000 ) ) ;
#12033=ORIENTED_EDGE ( 'NONE', *, *, #2822, .F. ) ;
#12043=ORIENTED_EDGE ( 'NONE', *, *, #5603, .F. ) ;
#12058=VECTOR ( 'NONE', #19054, 1000.000000000000000 ) ;
#12062=EDGE_CURVE ( 'NONE', #4579, #19119, #2996, .T. ) ;
#12066=CYLINDRICAL_SURFACE ( 'NONE', #34294, 7.199999999999993960 ) ;
#12072=ORIENTED_EDGE ( 'NONE', *, *, #25639, .T. ) ;
#12078=ORIENTED_EDGE ( 'NONE', *, *, #1342, .F. ) ;
#12080=DIRECTION ( 'NONE',  ( -1.000000000000000000, 0.000000000000000000, 0.000000000000000000 ) ) ;
#12086=VECTOR ( 'NONE', #19062, 1000.000000000000000 ) ;
#12092=DIRECTION ( 'NONE',  ( -1.000000000000000000, 0.000000000000000000, 0.000000000000000000 ) ) ;
#12109=AXIS2_PLACEMENT_3D ( 'NONE', #17942, #1757, #18121 ) ;
#12113=EDGE_CURVE ( 'NONE', #1241, #5458, #5431, .T. ) ;
#12124=DIRECTION ( 'NONE',  ( -1.000000000000000000, 0.000000000000000000, -0.000000000000000000 ) ) ;
#12128=DIRECTION ( 'NONE',  ( -1.000000000000000000, 0.000000000000000000, 0.000000000000000000 ) ) ;
#12152=CARTESIAN_POINT ( 'NONE',  ( 8.000000000000000000, 0.000000000000000000, 0.000000000000000000 ) ) ;
#12164=CARTESIAN_POINT ( 'NONE',  ( 0.000000000000000000, 0.000000000000000000, 0.000000000000000000 ) ) ;
#12168=VECTOR ( 'NONE', #8285, 1000.000000000000000 ) ;
#12180=LINE ( 'NONE', #23329, #11767 ) ;
#12194=VERTEX_POINT ( 'NONE', #6786 ) ;
#12195=DIRECTION ( 'NONE',  ( 0.000000000000000000, 0.9848077530122073542, 0.1736481776669339394 ) ) ;
#12219=ORIENTED_EDGE ( 'NONE', *, *, #30477, .F. ) ;
#12227=VECTOR ( 'NONE', #18641, 1000.000000000000000 ) ;
#12229=CIRCLE ( 'NONE', #28902, 7.199999999999992184 ) ;
#12238=CIRCLE ( 'NONE', #16823, 7.199999999999993072 ) ;
#12243=AXIS2_PLACEMENT_3D ( 'NONE', #33208, #33547, #17324 ) ;
#12247=CYLINDRICAL_SURFACE ( 'NONE', #5375, 19.99999999999998579 ) ;
#12259=EDGE_LOOP ( 'NONE', ( #22081, #20039, #22951, #527 ) ) ;
#12302=LINE ( 'NONE', #34461, #5254 ) ;
#12303=EDGE_CURVE ( 'NONE', #13869, #28836, #28312, .T. ) ;
#12330=CARTESIAN_POINT ( 'NONE',  ( 8.000000000000000000, -12.49559743815772528, -9.169462670380713831 ) ) ;
#12352=DIRECTION ( 'NONE',  ( -1.000000000000000000, 0.000000000000000000, 0.000000000000000000 ) ) ;
#12365=AXIS2_PLACEMENT_3D ( 'NONE', #5705, #22251, #33250 ) ;
#12404=DIRECTION ( 'NONE',  ( -1.000000000000000000, 0.000000000000000000, 0.000000000000000000 ) ) ;
#12407=AXIS2_PLACEMENT_3D ( 'NONE', #3758, #20284, #25546 ) ;
#12429=CIRCLE ( 'NONE', #13588, 19.99999999999998579 ) ;
#12465=CIRCLE ( 'NONE', #13071, 19.99999999999998579 ) ;
#12482=EDGE_LOOP ( 'NONE', ( #11374, #11257, #10372, #19567 ) ) ;
#12487=VECTOR ( 'NONE', #10417, 1000.000000000000000 ) ;
#12495=ORIENTED_EDGE ( 'NONE', *, *, #6406, .T. ) ;
#12538=CARTESIAN_POINT ( 'NONE',  ( 8.000000000000000000, 6.860320204751340079, -13.89802171851375689 ) ) ;
#12539=DIRECTION ( 'NONE',  ( 0.000000000000000000, 0.3420201433256629953, 0.9396926207859105373 ) ) ;
#12542=ORIENTED_EDGE ( 'NONE', *, *, #26421, .T. ) ;
#12543=CIRCLE ( 'NONE', #34398, 7.199999999999994849 ) ;
#12569=EDGE_CURVE ( 'NONE', #1645, #10783, #24179, .T. ) ;
#12570=DIRECTION ( 'NONE',  ( 1.000000000000000000, -0.000000000000000000, 0.000000000000000000 ) ) ;
#12591=FACE_OUTER_BOUND ( 'NONE', #9697, .T. ) ;
#12592=ADVANCED_FACE ( 'NONE', ( #35125 ), #21574, .T. ) ;
#12599=EDGE_CURVE ( 'NONE', #15022, #17024, #1633, .T. ) ;
#12608=DIRECTION ( 'NONE',  ( 0.000000000000000000, 0.000000000000000000, 1.000000000000000000 ) ) ;
#12615=CYLINDRICAL_SURFACE ( 'NONE', #890, 7.199999999999993960 ) ;
#12619=ORIENTED_EDGE ( 'NONE', *, *, #13652, .F. ) ;
#12624=CARTESIAN_POINT ( 'NONE',  ( 8.000000000000000000, 3.678165988948789877, -15.05623113391063406 ) ) ;
#12646=EDGE_CURVE ( 'NONE', #4835, #26059, #21939, .T. ) ;
#12650=VERTEX_POINT ( 'NONE', #5402 ) ;
#12718=( NAMED_UNIT ( * ) SI_UNIT ( $, .STERADIAN. ) SOLID_ANGLE_UNIT ( ) );
#12720=ORIENTED_EDGE ( 'NONE', *, *, #14319, .F. ) ;
#12725=DIRECTION ( 'NONE',  ( 0.000000000000000000, 0.000000000000000000, 1.000000000000000000 ) ) ;
#12726=VERTEX_POINT ( 'NONE', #2712 ) ;
#12749=LINE ( 'NONE', #12926, #34196 ) ;
#12757=VERTEX_POINT ( 'NONE', #3054 ) ;
#12782=CARTESIAN_POINT ( 'NONE',  ( 4.000000000000000000, 13.24207120356986422, -14.98824707027428005 ) ) ;
#12791=CARTESIAN_POINT ( 'NONE',  ( 0.000000000000000000, 16.71027810728552154, 4.579731798933998732 ) ) ;
#12794=CIRCLE ( 'NONE', #26599, 15.49899999999998101 ) ;
#12810=ORIENTED_EDGE ( 'NONE', *, *, #23357, .T. ) ;
#12817=EDGE_CURVE ( 'NONE', #18374, #10377, #30420, .T. ) ;
#12837=AXIS2_PLACEMENT_3D ( 'NONE', #18657, #27670, #19362 ) ;
#12856=DIRECTION ( 'NONE',  ( -1.000000000000000000, 0.000000000000000000, 0.000000000000000000 ) ) ;
#12862=AXIS2_PLACEMENT_3D ( 'NONE', #30050, #16333, #8244 ) ;
#12871=VECTOR ( 'NONE', #17185, 1000.000000000000000 ) ;
#12907=CARTESIAN_POINT ( 'NONE',  ( 8.000000000000000000, -6.860320204751044315, -13.89802171851389900 ) ) ;
#12916=ADVANCED_FACE ( 'NONE', ( #19925 ), #25371, .T. ) ;
#12926=CARTESIAN_POINT ( 'NONE',  ( 4.000000000000000000, -13.24207120356955159, -14.98824707027455183 ) ) ;
#12981=CIRCLE ( 'NONE', #31371, 19.99999999999998579 ) ;
#12986=DIRECTION ( 'NONE',  ( 1.000000000000000000, -0.000000000000000000, -0.000000000000000000 ) ) ;
#12989=ORIENTED_EDGE ( 'NONE', *, *, #27794, .F. ) ;
#12993=DIRECTION ( 'NONE',  ( 0.000000000000000000, 0.000000000000000000, 1.000000000000000000 ) ) ;
#12997=AXIS2_PLACEMENT_3D ( 'NONE', #23270, #31205, #22557 ) ;
#13006=EDGE_CURVE ( 'NONE', #18147, #1452, #25725, .T. ) ;
#13040=FILL_AREA_STYLE ('',( #2066 ) ) ;
#13057=EDGE_CURVE ( 'NONE', #23156, #28712, #13837, .T. ) ;
#13063=CIRCLE ( 'NONE', #33180, 7.199999999999993960 ) ;
#13070=EDGE_CURVE ( 'NONE', #27693, #14516, #32246, .T. ) ;
#13071=AXIS2_PLACEMENT_3D ( 'NONE', #10713, #26938, #5491 ) ;
#13084=AXIS2_PLACEMENT_3D ( 'NONE', #16248, #13401, #11055 ) ;
#13112=CARTESIAN_POINT ( 'NONE',  ( 8.000000000000000000, 0.000000000000000000, 0.000000000000000000 ) ) ;
#13119=LINE ( 'NONE', #26791, #18155 ) ;
#13121=CYLINDRICAL_SURFACE ( 'NONE', #22764, 19.99999999999998579 ) ;
#13126=DIRECTION ( 'NONE',  ( 0.000000000000000000, 0.000000000000000000, 1.000000000000000000 ) ) ;
#13128=ORIENTED_EDGE ( 'NONE', *, *, #12817, .F. ) ;
#13134=EDGE_CURVE ( 'NONE', #5612, #18458, #7511, .T. ) ;
#13160=CARTESIAN_POINT ( 'NONE',  ( 8.000000000000000000, -16.71027810728550733, -2.620268201066114688 ) ) ;
#13179=ORIENTED_EDGE ( 'NONE', *, *, #29883, .F. ) ;
#13183=ORIENTED_EDGE ( 'NONE', *, *, #1981, .F. ) ;
#13189=VERTEX_POINT ( 'NONE', #7510 ) ;
#13193=DIRECTION ( 'NONE',  ( -1.000000000000000000, 0.000000000000000000, 0.000000000000000000 ) ) ;
#13207=DIRECTION ( 'NONE',  ( 0.000000000000000000, 0.000000000000000000, 1.000000000000000000 ) ) ;
#13208=CIRCLE ( 'NONE', #17180, 15.49899999999998812 ) ;
#13217=ORIENTED_EDGE ( 'NONE', *, *, #22705, .F. ) ;
#13220=EDGE_CURVE ( 'NONE', #21073, #24111, #9799, .T. ) ;
#13222=SURFACE_STYLE_USAGE ( .BOTH. , #13563 ) ;
#13224=ORIENTED_EDGE ( 'NONE', *, *, #24076, .T. ) ;
#13255=DIRECTION ( 'NONE',  ( 0.000000000000000000, 0.000000000000000000, 1.000000000000000000 ) ) ;
#13263=EDGE_CURVE ( 'NONE', #23156, #12650, #26841, .T. ) ;
#13264=AXIS2_PLACEMENT_3D ( 'NONE', #13573, #34837, #26737 ) ;
#13269=AXIS2_PLACEMENT_3D ( 'NONE', #18849, #2485, #24793 ) ;
#13282=AXIS2_PLACEMENT_3D ( 'NONE', #20010, #17313, #24913 ) ;
#13286=EDGE_CURVE ( 'NONE', #26760, #21695, #28544, .T. ) ;
#13292=CARTESIAN_POINT ( 'NONE',  ( 8.000000000000000000, 12.49559743815794199, -9.169462670380459812 ) ) ;
#13301=VERTEX_POINT ( 'NONE', #5359 ) ;
#13340=ORIENTED_EDGE ( 'NONE', *, *, #18487, .T. ) ;
#13349=VERTEX_POINT ( 'NONE', #25866 ) ;
#13383=LINE ( 'NONE', #4935, #23963 ) ;
#13389=( NAMED_UNIT ( * ) PLANE_ANGLE_UNIT ( ) SI_UNIT ( $, .RADIAN. ) );
#13401=DIRECTION ( 'NONE',  ( -1.000000000000000000, 0.000000000000000000, 0.000000000000000000 ) ) ;
#13420=FACE_OUTER_BOUND ( 'NONE', #142, .T. ) ;
#13430=LINE ( 'NONE', #32500, #12227 ) ;
#13440=DIRECTION ( 'NONE',  ( -1.000000000000000000, 0.000000000000000000, 0.000000000000000000 ) ) ;
#13456=CARTESIAN_POINT ( 'NONE',  ( 8.000000000000000000, -10.62435788049434038, -13.16139124467930444 ) ) ;
#13460=CYLINDRICAL_SURFACE ( 'NONE', #1714, 7.199999999999993960 ) ;
#13464=CYLINDRICAL_SURFACE ( 'NONE', #27318, 7.199999999999993960 ) ;
#13479=ORIENTED_EDGE ( 'NONE', *, *, #13134, .F. ) ;
#13495=DIRECTION ( 'NONE',  ( -1.000000000000000000, 0.000000000000000000, 0.000000000000000000 ) ) ;
#13535=DIRECTION ( 'NONE',  ( -1.000000000000000000, 0.000000000000000000, 0.000000000000000000 ) ) ;
#13546=DIRECTION ( 'NONE',  ( 1.000000000000000000, -0.000000000000000000, -0.000000000000000000 ) ) ;
#13563=SURFACE_SIDE_STYLE ('',( #21295 ) ) ;
#13571=CARTESIAN_POINT ( 'NONE',  ( 0.000000000000000000, 16.59870953437680896, 3.253005020243904255 ) ) ;
#13573=CARTESIAN_POINT ( 'NONE',  ( 8.000000000000000000, 0.000000000000000000, 0.000000000000000000 ) ) ;
#13580=ORIENTED_EDGE ( 'NONE', *, *, #30877, .F. ) ;
#13586=CARTESIAN_POINT ( 'NONE',  ( 8.000000000000000000, 3.678165988948591814, 15.05623113391068379 ) ) ;
#13588=AXIS2_PLACEMENT_3D ( 'NONE', #17920, #4264, #1198 ) ;
#13595=DIRECTION ( 'NONE',  ( -1.000000000000000000, 0.000000000000000000, 0.000000000000000000 ) ) ;
#13610=VECTOR ( 'NONE', #18853, 1000.000000000000000 ) ;
#13645=LINE ( 'NONE', #13819, #3947 ) ;
#13652=EDGE_CURVE ( 'NONE', #10099, #31717, #30882, .T. ) ;
#13658=CARTESIAN_POINT ( 'NONE',  ( 8.000000000000000000, 0.000000000000000000, 0.000000000000000000 ) ) ;
#13687=EDGE_CURVE ( 'NONE', #10783, #10620, #10205, .T. ) ;
#13691=FACE_OUTER_BOUND ( 'NONE', #20883, .T. ) ;
#13692=DIRECTION ( 'NONE',  ( 0.000000000000000000, 0.000000000000000000, -1.000000000000000000 ) ) ;
#13704=EDGE_CURVE ( 'NONE', #11984, #21331, #29809, .T. ) ;
#13714=EDGE_CURVE ( 'NONE', #7443, #23156, #5147, .T. ) ;
#13727=EDGE_LOOP ( 'NONE', ( #11667, #23553, #1840, #22306 ) ) ;
#13733=EDGE_LOOP ( 'NONE', ( #23730, #9619, #18774, #33351 ) ) ;
#13737=EDGE_CURVE ( 'NONE', #20033, #7746, #28602, .T. ) ;
#13765=AXIS2_PLACEMENT_3D ( 'NONE', #5351, #22067, #16292 ) ;
#13777=CARTESIAN_POINT ( 'NONE',  ( 8.000000000000000000, -16.71027810728551799, 2.620268201065888203 ) ) ;
#13788=ORIENTED_EDGE ( 'NONE', *, *, #25774, .T. ) ;
#13811=ORIENTED_EDGE ( 'NONE', *, *, #2482, .F. ) ;
#13814=DIRECTION ( 'NONE',  ( -1.000000000000000000, 0.000000000000000000, 0.000000000000000000 ) ) ;
#13819=CARTESIAN_POINT ( 'NONE',  ( 0.000000000000000000, 0.000000000000000000, -1.000000000000000000 ) ) ;
#13835=ORIENTED_EDGE ( 'NONE', *, *, #30246, .T. ) ;
#13837=CIRCLE ( 'NONE', #23026, 7.199999999999994849 ) ;
#13855=VERTEX_POINT ( 'NONE', #21730 ) ;
#13860=CARTESIAN_POINT ( 'NONE',  ( 8.000000000000000000, 0.3212489022567689423, -16.91141623315866482 ) ) ;
#13869=VERTEX_POINT ( 'NONE', #35614 ) ;
#13910=ORIENTED_EDGE ( 'NONE', *, *, #29917, .T. ) ;
#13921=DIRECTION ( 'NONE',  ( -1.000000000000000000, 0.000000000000000000, 0.000000000000000000 ) ) ;
#13922=EDGE_CURVE ( 'NONE', #18458, #11984, #9605, .T. ) ;
#13934=ORIENTED_EDGE ( 'NONE', *, *, #13006, .T. ) ;
#13937=EDGE_CURVE ( 'NONE', #31771, #16680, #13063, .T. ) ;
#13944=CYLINDRICAL_SURFACE ( 'NONE', #9802, 19.99999999999998579 ) ;
#13949=ORIENTED_EDGE ( 'NONE', *, *, #33158, .F. ) ;
#13951=CARTESIAN_POINT ( 'NONE',  ( 8.000000000000000000, 14.87816164169121080, -4.342730381189718436 ) ) ;
#13960=EDGE_CURVE ( 'NONE', #656, #6464, #7521, .T. ) ;
#13976=DIRECTION ( 'NONE',  ( 1.000000000000000000, -0.000000000000000000, 0.000000000000000000 ) ) ;
#13980=ORIENTED_EDGE ( 'NONE', *, *, #27077, .T. ) ;
#13990=FACE_OUTER_BOUND ( 'NONE', #13727, .T. ) ;
#14009=CARTESIAN_POINT ( 'NONE',  ( 4.000000000000000000, -19.60123832284022782, 3.973846525876368219 ) ) ;
#14036=ORIENTED_EDGE ( 'NONE', *, *, #637, .T. ) ;
#14053=AXIS2_PLACEMENT_3D ( 'NONE', #16679, #306, #19551 ) ;
#14054=CIRCLE ( 'NONE', #5470, 15.49899999999998457 ) ;
#14060=VERTEX_POINT ( 'NONE', #22785 ) ;
#14067=EDGE_CURVE ( 'NONE', #1452, #31709, #29770, .T. ) ;
#14073=ORIENTED_EDGE ( 'NONE', *, *, #15260, .T. ) ;
#14103=CARTESIAN_POINT ( 'NONE',  ( 4.000000000000000000, -19.60123832284014611, -3.973846525876633340 ) ) ;
#14107=DIRECTION ( 'NONE',  ( 0.000000000000000000, 0.000000000000000000, 1.000000000000000000 ) ) ;
#14110=CARTESIAN_POINT ( 'NONE',  ( 0.000000000000000000, -1.693188892523841194, 15.40623615209871389 ) ) ;
#14111=EDGE_CURVE ( 'NONE', #1026, #28288, #17573, .T. ) ;
#14115=EDGE_CURVE ( 'NONE', #1605, #18539, #6105, .T. ) ;
#14119=EDGE_LOOP ( 'NONE', ( #19946, #4452, #2414, #30942 ) ) ;
#14124=ORIENTED_EDGE ( 'NONE', *, *, #16571, .T. ) ;
#14129=DIRECTION ( 'NONE',  ( 1.000000000000000000, -0.000000000000000000, 0.000000000000000000 ) ) ;
#14166=VECTOR ( 'NONE', #24622, 1000.000000000000000 ) ;
#14182=CIRCLE ( 'NONE', #19370, 15.49900000000000233 ) ;
#14186=CIRCLE ( 'NONE', #18790, 19.99999999999998579 ) ;
#14201=CYLINDRICAL_SURFACE ( 'NONE', #15770, 7.199999999999993960 ) ;
#14207=DIRECTION ( 'NONE',  ( 0.000000000000000000, 0.6427876096865349220, 0.7660444431189816772 ) ) ;
#14209=AXIS2_PLACEMENT_3D ( 'NONE', #31952, #7288, #15549 ) ;
#14241=CARTESIAN_POINT ( 'NONE',  ( 8.000000000000000000, 11.11653975335790179, 12.74840161668735661 ) ) ;
#14242=ORIENTED_EDGE ( 'NONE', *, *, #5842, .T. ) ;
#14262=VERTEX_POINT ( 'NONE', #20965 ) ;
#14291=CARTESIAN_POINT ( 'NONE',  ( 8.000000000000000000, 3.872983346207417021, -1.000000000000000000 ) ) ;
#14317=DIRECTION ( 'NONE',  ( 0.000000000000000000, 0.000000000000000000, 1.000000000000000000 ) ) ;
#14319=EDGE_CURVE ( 'NONE', #6685, #26059, #12429, .T. ) ;
#14324=EDGE_CURVE ( 'NONE', #13189, #20288, #23509, .T. ) ;
#14371=EDGE_CURVE ( 'NONE', #14262, #27701, #15286, .T. ) ;
#14377=DIRECTION ( 'NONE',  ( -1.000000000000000000, 0.000000000000000000, 0.000000000000000000 ) ) ;
#14381=EDGE_LOOP ( 'NONE', ( #17117, #32606, #7444, #21515 ) ) ;
#14382=ORIENTED_EDGE ( 'NONE', *, *, #13922, .T. ) ;
#14398=LINE ( 'NONE', #11701, #3908 ) ;
#14413=VERTEX_POINT ( 'NONE', #18815 ) ;
#14430=ORIENTED_EDGE ( 'NONE', *, *, #9857, .T. ) ;
#14432=DIRECTION ( 'NONE',  ( 0.000000000000000000, 0.6427876096865403621, -0.7660444431189772363 ) ) ;
#14436=ADVANCED_FACE ( 'NONE', ( #18993 ), #26759, .T. ) ;
#14451=LINE ( 'NONE', #14103, #34114 ) ;
#14455=DIRECTION ( 'NONE',  ( -1.000000000000000000, 0.000000000000000000, 0.000000000000000000 ) ) ;
#14475=DIRECTION ( 'NONE',  ( -1.000000000000000000, 0.000000000000000000, 0.000000000000000000 ) ) ;
#14495=DIRECTION ( 'NONE',  ( -1.000000000000000000, 0.000000000000000000, 0.000000000000000000 ) ) ;
#14508=PRODUCT_CONTEXT ( 'NONE', #9172, 'mechanical' ) ;
#14516=VERTEX_POINT ( 'NONE', #14110 ) ;
#14548=DIRECTION ( 'NONE',  ( 0.000000000000000000, 0.000000000000000000, 1.000000000000000000 ) ) ;
#14550=EDGE_CURVE ( 'NONE', #24079, #22597, #16810, .T. ) ;
#14551=ORIENTED_EDGE ( 'NONE', *, *, #15496, .F. ) ;
#14561=CIRCLE ( 'NONE', #17446, 7.199999999999994849 ) ;
#14564=ADVANCED_FACE ( 'NONE', ( #33738 ), #33216, .T. ) ;
#14570=DIRECTION ( 'NONE',  ( -1.000000000000000000, 0.000000000000000000, 0.000000000000000000 ) ) ;
#14582=CYLINDRICAL_SURFACE ( 'NONE', #27587, 19.99999999999998579 ) ;
#14583=CARTESIAN_POINT ( 'NONE',  ( 8.000000000000000000, 0.000000000000000000, 0.000000000000000000 ) ) ;
#14599=ORIENTED_EDGE ( 'NONE', *, *, #3170, .F. ) ;
#14600=DIRECTION ( 'NONE',  ( 0.000000000000000000, 0.000000000000000000, 1.000000000000000000 ) ) ;
#14601=DIRECTION ( 'NONE',  ( -1.000000000000000000, 0.000000000000000000, 0.000000000000000000 ) ) ;
#14618=CIRCLE ( 'NONE', #3804, 19.99999999999998579 ) ;
#14681=CARTESIAN_POINT ( 'NONE',  ( 8.000000000000000000, 0.000000000000000000, 0.000000000000000000 ) ) ;
#14711=EDGE_CURVE ( 'NONE', #28836, #2106, #25099, .T. ) ;
#14712=CARTESIAN_POINT ( 'NONE',  ( 8.000000000000000000, -8.605879768205133118, -12.89022243466717299 ) ) ;
#14714=DIRECTION ( 'NONE',  ( 0.000000000000000000, -0.3420201433256564449, -0.9396926207859127578 ) ) ;
#14724=ORIENTED_EDGE ( 'NONE', *, *, #33629, .T. ) ;
#14756=CARTESIAN_POINT ( 'NONE',  ( 8.000000000000000000, -14.80634052301617309, -8.177498406287382338 ) ) ;
#14773=AXIS2_PLACEMENT_3D ( 'NONE', #16499, #13814, #3195 ) ;
#14799=EDGE_CURVE ( 'NONE', #9468, #21073, #2747, .T. ) ;
#14800=CARTESIAN_POINT ( 'NONE',  ( 4.000000000000000000, -0.5097555531874695678, 19.99350267651955093 ) ) ;
#14819=ORIENTED_EDGE ( 'NONE', *, *, #2527, .F. ) ;
#14823=LINE ( 'NONE', #28697, #16701 ) ;
#14826=CARTESIAN_POINT ( 'NONE',  ( 8.000000000000000000, 0.000000000000000000, 0.000000000000000000 ) ) ;
#14829=CYLINDRICAL_SURFACE ( 'NONE', #35449, 15.49899999999998457 ) ;
#14847=DIRECTION ( 'NONE',  ( 0.000000000000000000, -0.8660254037844432595, 0.4999999999999918954 ) ) ;
#14880=CARTESIAN_POINT ( 'NONE',  ( 8.000000000000000000, 0.000000000000000000, 0.000000000000000000 ) ) ;
#14886=DIRECTION ( 'NONE',  ( -1.000000000000000000, 0.000000000000000000, 0.000000000000000000 ) ) ;
#14891=CARTESIAN_POINT ( 'NONE',  ( 4.000000000000000000, 0.5097555531875970214, -19.99350267651952606 ) ) ;
#14930=AXIS2_PLACEMENT_3D ( 'NONE', #32327, #5333, #5160 ) ;
#14944=DIRECTION ( 'NONE',  ( -1.000000000000000000, 0.000000000000000000, 0.000000000000000000 ) ) ;
#14957=DIRECTION ( 'NONE',  ( -1.000000000000000000, 0.000000000000000000, 0.000000000000000000 ) ) ;
#14959=AXIS2_PLACEMENT_3D ( 'NONE', #24850, #7, #27566 ) ;
#14967=EDGE_LOOP ( 'NONE', ( #13910, #34784, #29325, #6871, #6248, #21275, #31355, #20827, #24990, #9725, #25472, #20407, #11476, #20776, #2068, #29154, #1420, #24414, #24529, #18027, #29209, #16638, #10000, #14242, #28859, #28210, #20353, #31567, #2859, #35097, #35404, #4926, #10472, #6200, #29457, #1103, #24470, #26761, #21959, #32467, #12619, #18761, #23575, #11019, #13580, #27866, #8547, #90, #8549, #22522, #2295, #32073, #34072, #14989, #31278, #26399, #3204, #8590, #4110, #27235, #17760, #14124, #9032, #4192, #3398, #20756, #12078, #21058, #14036, #11349, #35500, #5665, #8233, #33376, #17386, #31437, #3110 ) ) ;
#14989=ORIENTED_EDGE ( 'NONE', *, *, #13937, .F. ) ;
#15002=ORIENTED_EDGE ( 'NONE', *, *, #6405, .F. ) ;
#15010=MECHANICAL_DESIGN_GEOMETRIC_PRESENTATION_REPRESENTATION('',(#15570),#2402);
#15012=DIRECTION ( 'NONE',  ( -1.000000000000000000, 0.000000000000000000, 0.000000000000000000 ) ) ;
#15022=VERTEX_POINT ( 'NONE', #27777 ) ;
#15035=AXIS2_PLACEMENT_3D ( 'NONE', #11475, #8760, #6074 ) ;
#15038=EDGE_LOOP ( 'NONE', ( #8367, #29641, #10086, #7326 ) ) ;
#15041=EDGE_LOOP ( 'NONE', ( #27680, #35322, #21381, #34651 ) ) ;
#15087=ORIENTED_EDGE ( 'NONE', *, *, #11251, .F. ) ;
#15108=CARTESIAN_POINT ( 'NONE',  ( 8.000000000000000000, -5.482169781018729537, -16.00140663693126086 ) ) ;
#15143=CIRCLE ( 'NONE', #23203, 15.49899999999998457 ) ;
#15164=ORIENTED_EDGE ( 'NONE', *, *, #7459, .F. ) ;
#15175=ORIENTED_EDGE ( 'NONE', *, *, #10163, .T. ) ;
#15178=EDGE_CURVE ( 'NONE', #7873, #11499, #5578, .T. ) ;
#15191=LINE ( 'NONE', #34671, #20489 ) ;
#15197=AXIS2_PLACEMENT_3D ( 'NONE', #15962, #24268, #10755 ) ;
#15218=DIRECTION ( 'NONE',  ( -1.000000000000000000, 0.000000000000000000, 0.000000000000000000 ) ) ;
#15243=ADVANCED_FACE ( 'NONE', ( #31357 ), #9390, .T. ) ;
#15260=EDGE_CURVE ( 'NONE', #28836, #14516, #7040, .T. ) ;
#15286=CIRCLE ( 'NONE', #35443, 7.199999999999994849 ) ;
#15290=ORIENTED_EDGE ( 'NONE', *, *, #6279, .T. ) ;
#15298=ORIENTED_EDGE ( 'NONE', *, *, #14711, .T. ) ;
#15314=ORIENTED_EDGE ( 'NONE', *, *, #16324, .T. ) ;
#15329=CARTESIAN_POINT ( 'NONE',  ( 4.000000000000000000, 6.359167119270465740, 18.96209359615096446 ) ) ;
#15330=ADVANCED_FACE ( 'NONE', ( #9749 ), #25613, .T. ) ;
#15335=DIRECTION ( 'NONE',  ( -1.000000000000000000, 0.000000000000000000, 0.000000000000000000 ) ) ;
#15343=EDGE_CURVE ( 'NONE', #984, #14262, #934, .T. ) ;
#15366=CARTESIAN_POINT ( 'NONE',  ( 8.000000000000000000, 16.59870953437680896, 3.253005020243904255 ) ) ;
#15375=ORIENTED_EDGE ( 'NONE', *, *, #11387, .F. ) ;
#15391=AXIS2_PLACEMENT_3D ( 'NONE', #16514, #3034, #32915 ) ;
#15440=AXIS2_PLACEMENT_3D ( 'NONE', #4065, #15012, #17891 ) ;
#15480=CARTESIAN_POINT ( 'NONE',  ( 8.000000000000000000, -19.77827456857333743, -2.969824084036674527 ) ) ;
#15496=EDGE_CURVE ( 'NONE', #34524, #31265, #25389, .T. ) ;
#15528=ORIENTED_EDGE ( 'NONE', *, *, #6405, .T. ) ;
#15549=DIRECTION ( 'NONE',  ( 0.000000000000000000, -0.8660254037844432595, 0.4999999999999920619 ) ) ;
#15550=CARTESIAN_POINT ( 'NONE',  ( 0.000000000000000000, -14.18878633068154826, -6.236773481718229206 ) ) ;
#15563=VERTEX_POINT ( 'NONE', #30261 ) ;
#15570=STYLED_ITEM ( 'NONE', ( #5295 ), #1766 ) ;
#15587=FACE_OUTER_BOUND ( 'NONE', #22876, .T. ) ;
#15593=DIRECTION ( 'NONE',  ( 0.000000000000000000, 0.9848077530122085754, -0.1736481776669275556 ) ) ;
#15623=FACE_OUTER_BOUND ( 'NONE', #840, .T. ) ;
#15628=EDGE_CURVE ( 'NONE', #6999, #26953, #16504, .T. ) ;
#15639=ORIENTED_EDGE ( 'NONE', *, *, #35414, .F. ) ;
#15664=EDGE_CURVE ( 'NONE', #14413, #26963, #31476, .T. ) ;
#15700=CIRCLE ( 'NONE', #20290, 7.199999999999993960 ) ;
#15719=AXIS2_PLACEMENT_3D ( 'NONE', #19075, #32590, #13692 ) ;
#15721=CIRCLE ( 'NONE', #10578, 7.199999999999992184 ) ;
#15726=DIRECTION ( 'NONE',  ( 0.000000000000000000, 0.000000000000000000, 1.000000000000000000 ) ) ;
#15744=CIRCLE ( 'NONE', #33015, 7.199999999999995737 ) ;
#15754=DIRECTION ( 'NONE',  ( -1.000000000000000000, 0.000000000000000000, 0.000000000000000000 ) ) ;
#15766=DIRECTION ( 'NONE',  ( -1.000000000000000000, 0.000000000000000000, 0.000000000000000000 ) ) ;
#15770=AXIS2_PLACEMENT_3D ( 'NONE', #11156, #27202, #8618 ) ;
#15779=CARTESIAN_POINT ( 'NONE',  ( 0.000000000000000000, -19.60123832284022782, 3.973846525876367330 ) ) ;
#15786=ADVANCED_FACE ( 'NONE', ( #12591 ), #35275, .T. ) ;
#15791=AXIS2_PLACEMENT_3D ( 'NONE', #12164, #6938, #20066 ) ;
#15805=VECTOR ( 'NONE', #21448, 1000.000000000000000 ) ;
#15813=CARTESIAN_POINT ( 'NONE',  ( 8.000000000000000000, -14.87816164169111310, -4.342730381190021305 ) ) ;
#15818=AXIS2_PLACEMENT_3D ( 'NONE', #25992, #12124, #3679 ) ;
#15835=APPLICATION_CONTEXT ( 'automotive_design' ) ;
#15839=ORIENTED_EDGE ( 'NONE', *, *, #8025, .F. ) ;
#15844=ORIENTED_EDGE ( 'NONE', *, *, #448, .F. ) ;
#15865=EDGE_CURVE ( 'NONE', #2544, #32647, #29794, .T. ) ;
#15890=CIRCLE ( 'NONE', #7267, 15.49899999999998457 ) ;
#15901=EDGE_CURVE ( 'NONE', #33477, #5642, #34967, .T. ) ;
#15910=EDGE_CURVE ( 'NONE', #21654, #28712, #24039, .T. ) ;
#15919=VERTEX_POINT ( 'NONE', #16860 ) ;
#15922=CARTESIAN_POINT ( 'NONE',  ( 8.000000000000000000, -16.59870953437678409, -3.253005020244019718 ) ) ;
#15940=CARTESIAN_POINT ( 'NONE',  ( 8.000000000000000000, 0.000000000000000000, 0.000000000000000000 ) ) ;
#15943=ADVANCED_FACE ( 'NONE', ( #24987 ), #11304, .T. ) ;
#15949=DIRECTION ( 'NONE',  ( 0.000000000000000000, 0.000000000000000000, 1.000000000000000000 ) ) ;
#15962=CARTESIAN_POINT ( 'NONE',  ( 0.000000000000000000, -16.71027810728550733, -2.620268201066114688 ) ) ;
#15964=CARTESIAN_POINT ( 'NONE',  ( 0.000000000000000000, 16.71027810728549667, 2.620268201066223934 ) ) ;
#16021=DIRECTION ( 'NONE',  ( 0.000000000000000000, 0.000000000000000000, -1.000000000000000000 ) ) ;
#16029=ORIENTED_EDGE ( 'NONE', *, *, #5122, .F. ) ;
#16042=DIRECTION ( 'NONE',  ( 0.000000000000000000, 0.000000000000000000, 1.000000000000000000 ) ) ;
#16048=DIRECTION ( 'NONE',  ( 0.000000000000000000, 0.8660254037844363761, 0.5000000000000037748 ) ) ;
#16086=DIRECTION ( 'NONE',  ( 0.000000000000000000, 0.3420201433256693235, -0.9396926207859082059 ) ) ;
#16092=CYLINDRICAL_SURFACE ( 'NONE', #28779, 7.199999999999994849 ) ;
#16099=CARTESIAN_POINT ( 'NONE',  ( 8.000000000000000000, 6.085920226791021292, 15.78165944574522861 ) ) ;
#16106=ORIENTED_EDGE ( 'NONE', *, *, #28201, .F. ) ;
#16124=VECTOR ( 'NONE', #18165, 1000.000000000000000 ) ;
#16149=DIRECTION ( 'NONE',  ( -1.000000000000000000, 0.000000000000000000, 0.000000000000000000 ) ) ;
#16189=DIRECTION ( 'NONE',  ( -1.000000000000000000, 0.000000000000000000, 0.000000000000000000 ) ) ;
#16192=ORIENTED_EDGE ( 'NONE', *, *, #21430, .F. ) ;
#16212=VERTEX_POINT ( 'NONE', #26411 ) ;
#16214=CYLINDRICAL_SURFACE ( 'NONE', #21424, 15.49899999999998457 ) ;
#16222=CARTESIAN_POINT ( 'NONE',  ( 0.000000000000000000, 6.085920226791238008, -15.78165944574512203 ) ) ;
#16229=VECTOR ( 'NONE', #8001, 1000.000000000000000 ) ;
#16248=CARTESIAN_POINT ( 'NONE',  ( 8.000000000000000000, -14.80634052301628145, 8.177498406287162069 ) ) ;
#16261=ORIENTED_EDGE ( 'NONE', *, *, #25743, .F. ) ;
#16264=EDGE_CURVE ( 'NONE', #11433, #27701, #34696, .T. ) ;
#16278=ORIENTED_EDGE ( 'NONE', *, *, #8841, .F. ) ;
#16283=ORIENTED_EDGE ( 'NONE', *, *, #19016, .F. ) ;
#16292=DIRECTION ( 'NONE',  ( 0.000000000000000000, 0.000000000000000000, 1.000000000000000000 ) ) ;
#16324=EDGE_CURVE ( 'NONE', #12726, #12194, #22186, .T. ) ;
#16333=DIRECTION ( 'NONE',  ( -1.000000000000000000, 0.000000000000000000, 0.000000000000000000 ) ) ;
#16338=AXIS2_PLACEMENT_3D ( 'NONE', #3237, #27555, #2894 ) ;
#16340=ADVANCED_FACE ( 'NONE', ( #3658 ), #27792, .T. ) ;
#16354=DIRECTION ( 'NONE',  ( 0.000000000000000000, 0.000000000000000000, 1.000000000000000000 ) ) ;
#16361=ORIENTED_EDGE ( 'NONE', *, *, #25729, .F. ) ;
#16364=AXIS2_PLACEMENT_3D ( 'NONE', #16710, #333, #11329 ) ;
#16369=CARTESIAN_POINT ( 'NONE',  ( 8.000000000000000000, 0.000000000000000000, 0.000000000000000000 ) ) ;
#16384=EDGE_CURVE ( 'NONE', #14413, #28288, #20008, .T. ) ;
#16387=CARTESIAN_POINT ( 'NONE',  ( 8.000000000000000000, 1.693188892523745936, 15.40623615209872632 ) ) ;
#16403=ORIENTED_EDGE ( 'NONE', *, *, #13652, .T. ) ;
#16447=DIRECTION ( 'NONE',  ( -1.000000000000000000, 0.000000000000000000, 0.000000000000000000 ) ) ;
#16456=DIRECTION ( 'NONE',  ( -1.000000000000000000, 0.000000000000000000, 0.000000000000000000 ) ) ;
#16461=CARTESIAN_POINT ( 'NONE',  ( 8.000000000000000000, 6.085920226791238008, -15.78165944574512203 ) ) ;
#16477=EDGE_CURVE ( 'NONE', #5366, #33371, #24645, .T. ) ;
#16488=DIRECTION ( 'NONE',  ( -1.000000000000000000, 0.000000000000000000, 0.000000000000000000 ) ) ;
#16499=CARTESIAN_POINT ( 'NONE',  ( 8.000000000000000000, -14.80634052301617309, -8.177498406287382338 ) ) ;
#16504=CIRCLE ( 'NONE', #5608, 19.99999999999998579 ) ;
#16508=AXIS2_PLACEMENT_3D ( 'NONE', #35382, #10710, #7818 ) ;
#16514=CARTESIAN_POINT ( 'NONE',  ( 0.000000000000000000, 0.000000000000000000, 0.000000000000000000 ) ) ;
#16516=DIRECTION ( 'NONE',  ( 0.000000000000000000, 0.000000000000000000, 1.000000000000000000 ) ) ;
#16527=DIRECTION ( 'NONE',  ( 0.000000000000000000, -0.3420201433256758738, 0.9396926207859057634 ) ) ;
#16565=VECTOR ( 'NONE', #14377, 1000.000000000000000 ) ;
#16571=EDGE_CURVE ( 'NONE', #876, #4835, #17160, .T. ) ;
#16609=ORIENTED_EDGE ( 'NONE', *, *, #15865, .F. ) ;
#16620=CARTESIAN_POINT ( 'NONE',  ( 8.000000000000000000, 19.77827456857338007, 2.969824084036535528 ) ) ;
#16624=AXIS2_PLACEMENT_3D ( 'NONE', #2652, #29479, #2307 ) ;
#16638=ORIENTED_EDGE ( 'NONE', *, *, #22179, .T. ) ;
#16659=CARTESIAN_POINT ( 'NONE',  ( 0.000000000000000000, 11.19999565274264519, -10.71350075272062519 ) ) ;
#16664=DIRECTION ( 'NONE',  ( 0.000000000000000000, 0.000000000000000000, 1.000000000000000000 ) ) ;
#16669=AXIS2_PLACEMENT_3D ( 'NONE', #10345, #29613, #21133 ) ;
#16673=DIRECTION ( 'NONE',  ( -1.000000000000000000, 0.000000000000000000, 0.000000000000000000 ) ) ;
#16679=CARTESIAN_POINT ( 'NONE',  ( 8.000000000000000000, 0.000000000000000000, 0.000000000000000000 ) ) ;
#16680=VERTEX_POINT ( 'NONE', #23293 ) ;
#16681=ADVANCED_FACE ( 'NONE', ( #9623 ), #31586, .T. ) ;
#16693=AXIS2_PLACEMENT_3D ( 'NONE', #16786, #8331, #30838 ) ;
#16701=VECTOR ( 'NONE', #25827, 1000.000000000000000 ) ;
#16710=CARTESIAN_POINT ( 'NONE',  ( 8.000000000000000000, 0.000000000000000000, 0.000000000000000000 ) ) ;
#16712=FACE_OUTER_BOUND ( 'NONE', #206, .T. ) ;
#16735=VERTEX_POINT ( 'NONE', #6918 ) ;
#16740=ORIENTED_EDGE ( 'NONE', *, *, #23566, .F. ) ;
#16752=EDGE_CURVE ( 'NONE', #17047, #16735, #7417, .T. ) ;
#16754=ADVANCED_FACE ( 'NONE', ( #28889 ), #26186, .T. ) ;
#16776=CARTESIAN_POINT ( 'NONE',  ( 8.000000000000000000, 6.085920226791021292, 15.78165944574522861 ) ) ;
#16786=CARTESIAN_POINT ( 'NONE',  ( 8.000000000000000000, -0.3212489022564151142, -16.91141623315864706 ) ) ;
#16804=DIRECTION ( 'NONE',  ( -1.000000000000000000, 0.000000000000000000, 0.000000000000000000 ) ) ;
#16810=LINE ( 'NONE', #30863, #34885 ) ;
#16823=AXIS2_PLACEMENT_3D ( 'NONE', #25280, #22736, #17152 ) ;
#16829=DIRECTION ( 'NONE',  ( 0.000000000000000000, 0.6427876096865349220, 0.7660444431189816772 ) ) ;
#16830=AXIS2_PLACEMENT_3D ( 'NONE', #6909, #20208, #3512 ) ;
#16853=VECTOR ( 'NONE', #31164, 1000.000000000000000 ) ;
#16859=CYLINDRICAL_SURFACE ( 'NONE', #34801, 7.199999999999994849 ) ;
#16860=CARTESIAN_POINT ( 'NONE',  ( 0.000000000000000000, -17.06000345190431844, -10.43821259704038695 ) ) ;
#16871=VECTOR ( 'NONE', #5931, 1000.000000000000000 ) ;
#16880=FACE_OUTER_BOUND ( 'NONE', #31186, .T. ) ;
#16891=VERTEX_POINT ( 'NONE', #5131 ) ;
#16894=ORIENTED_EDGE ( 'NONE', *, *, #13263, .F. ) ;
#16912=CARTESIAN_POINT ( 'NONE',  ( 8.000000000000000000, 14.18878633068169925, -6.236773481717946765 ) ) ;
#16918=CARTESIAN_POINT ( 'NONE',  ( 0.000000000000000000, 0.000000000000000000, 0.000000000000000000 ) ) ;
#16925=CARTESIAN_POINT ( 'NONE',  ( 0.000000000000000000, 0.5097555531873385615, 19.99350267651958291 ) ) ;
#16949=AXIS2_PLACEMENT_3D ( 'NONE', #20601, #1720, #4254 ) ;
#16987=ORIENTED_EDGE ( 'NONE', *, *, #2408, .T. ) ;
#17024=VERTEX_POINT ( 'NONE', #20181 ) ;
#17035=EDGE_CURVE ( 'NONE', #7160, #14413, #2961, .T. ) ;
#17047=VERTEX_POINT ( 'NONE', #11573 ) ;
#17048=CARTESIAN_POINT ( 'NONE',  ( 0.000000000000000000, -16.71027810728551799, 2.620268201065888203 ) ) ;
#17063=DIRECTION ( 'NONE',  ( -1.000000000000000000, 0.000000000000000000, 0.000000000000000000 ) ) ;
#17073=ORIENTED_EDGE ( 'NONE', *, *, #25303, .T. ) ;
#17081=CARTESIAN_POINT ( 'NONE',  ( 8.000000000000000000, 0.000000000000000000, -1.000000000000000000 ) ) ;
#17085=ORIENTED_EDGE ( 'NONE', *, *, #19643, .F. ) ;
#17107=CARTESIAN_POINT ( 'NONE',  ( 0.000000000000000000, -11.19999565274241782, -10.71350075272084545 ) ) ;
#17117=ORIENTED_EDGE ( 'NONE', *, *, #8305, .F. ) ;
#17152=DIRECTION ( 'NONE',  ( 0.000000000000000000, 0.3420201433256695456, -0.9396926207859079838 ) ) ;
#17160=CIRCLE ( 'NONE', #33862, 19.99999999999998579 ) ;
#17180=AXIS2_PLACEMENT_3D ( 'NONE', #20051, #6389, #16829 ) ;
#17185=DIRECTION ( 'NONE',  ( -1.000000000000000000, 0.000000000000000000, 0.000000000000000000 ) ) ;
#17193=EDGE_CURVE ( 'NONE', #2106, #4854, #20723, .T. ) ;
#17195=DIRECTION ( 'NONE',  ( 0.000000000000000000, 0.000000000000000000, 1.000000000000000000 ) ) ;
#17223=ORIENTED_EDGE ( 'NONE', *, *, #5381, .T. ) ;
#17229=CIRCLE ( 'NONE', #16669, 19.99999999999998579 ) ;
#17241=ORIENTED_EDGE ( 'NONE', *, *, #32117, .T. ) ;
#17286=CARTESIAN_POINT ( 'NONE',  ( 8.000000000000000000, 16.71027810728552154, -2.620268201066000113 ) ) ;
#17292=DIRECTION ( 'NONE',  ( -1.000000000000000000, 0.000000000000000000, 0.000000000000000000 ) ) ;
#17303=CARTESIAN_POINT ( 'NONE',  ( -10.00000000000000000, 0.000000000000000000, 0.000000000000000000 ) ) ;
#17304=DIRECTION ( 'NONE',  ( -1.000000000000000000, 0.000000000000000000, 0.000000000000000000 ) ) ;
#17309=ORIENTED_EDGE ( 'NONE', *, *, #4238, .T. ) ;
#17310=ORIENTED_EDGE ( 'NONE', *, *, #18487, .F. ) ;
#17313=DIRECTION ( 'NONE',  ( 0.000000000000000000, -1.000000000000000000, 0.000000000000000000 ) ) ;
#17319=DIRECTION ( 'NONE',  ( -1.000000000000000000, 0.000000000000000000, 0.000000000000000000 ) ) ;
#17324=DIRECTION ( 'NONE',  ( 0.000000000000000000, 0.9848077530122073542, 0.1736481776669339117 ) ) ;
#17325=ORIENTED_EDGE ( 'NONE', *, *, #14115, .F. ) ;
#17326=DIRECTION ( 'NONE',  ( -1.000000000000000000, 0.000000000000000000, 0.000000000000000000 ) ) ;
#17340=ORIENTED_EDGE ( 'NONE', *, *, #5838, .T. ) ;
#17352=VECTOR ( 'NONE', #18405, 1000.000000000000000 ) ;
#17359=AXIS2_PLACEMENT_3D ( 'NONE', #21616, #27053, #29399 ) ;
#17379=VERTEX_POINT ( 'NONE', #21033 ) ;
#17386=ORIENTED_EDGE ( 'NONE', *, *, #26139, .T. ) ;
#17417=VECTOR ( 'NONE', #5869, 1000.000000000000000 ) ;
#17429=ORIENTED_EDGE ( 'NONE', *, *, #33586, .T. ) ;
#17431=AXIS2_PLACEMENT_3D ( 'NONE', #10604, #21560, #32558 ) ;
#17446=AXIS2_PLACEMENT_3D ( 'NONE', #28497, #1485, #31722 ) ;
#17465=ORIENTED_EDGE ( 'NONE', *, *, #2482, .T. ) ;
#17481=DIRECTION ( 'NONE',  ( 0.000000000000000000, 0.000000000000000000, 1.000000000000000000 ) ) ;
#17483=EDGE_CURVE ( 'NONE', #20473, #32241, #10789, .T. ) ;
#17517=CIRCLE ( 'NONE', #33043, 15.49899999999999878 ) ;
#17525=ORIENTED_EDGE ( 'NONE', *, *, #3980, .T. ) ;
#17528=EDGE_CURVE ( 'NONE', #13301, #26725, #33910, .T. ) ;
#17533=EDGE_CURVE ( 'NONE', #17024, #8057, #5748, .T. ) ;
#17547=LINE ( 'NONE', #641, #10720 ) ;
#17559=ORIENTED_EDGE ( 'NONE', *, *, #26139, .F. ) ;
#17573=CIRCLE ( 'NONE', #25076, 19.99999999999998579 ) ;
#17601=AXIS2_PLACEMENT_3D ( 'NONE', #8707, #19676, #27474 ) ;
#17616=CYLINDRICAL_SURFACE ( 'NONE', #24801, 19.99999999999998579 ) ;
#17618=VERTEX_POINT ( 'NONE', #11650 ) ;
#17674=ORIENTED_EDGE ( 'NONE', *, *, #27958, .T. ) ;
#17679=ORIENTED_EDGE ( 'NONE', *, *, #28358, .T. ) ;
#17686=AXIS2_PLACEMENT_3D ( 'NONE', #34557, #12404, #14548 ) ;
#17692=VECTOR ( 'NONE', #27730, 1000.000000000000000 ) ;
#17709=AXIS2_PLACEMENT_3D ( 'NONE', #18885, #7717, #29880 ) ;
#17745=DIRECTION ( 'NONE',  ( 0.000000000000000000, 0.000000000000000000, 1.000000000000000000 ) ) ;
#17760=ORIENTED_EDGE ( 'NONE', *, *, #11048, .T. ) ;
#17781=AXIS2_PLACEMENT_3D ( 'NONE', #26823, #2176, #322 ) ;
#17818=EDGE_LOOP ( 'NONE', ( #11548, #1851, #28961, #14073 ) ) ;
#17840=AXIS2_PLACEMENT_3D ( 'NONE', #19846, #6195, #33734 ) ;
#17841=AXIS2_PLACEMENT_3D ( 'NONE', #176, #27384, #8458 ) ;
#17862=PLANE ( 'NONE',  #25006 ) ;
#17891=DIRECTION ( 'NONE',  ( 0.000000000000000000, 0.8660254037844398178, -0.4999999999999981681 ) ) ;
#17913=CARTESIAN_POINT ( 'NONE',  ( 4.000000000000000000, 17.56975900509174693, 9.555290079479316745 ) ) ;
#17920=CARTESIAN_POINT ( 'NONE',  ( 8.000000000000000000, 0.000000000000000000, 0.000000000000000000 ) ) ;
#17937=CARTESIAN_POINT ( 'NONE',  ( 8.000000000000000000, 0.000000000000000000, 0.000000000000000000 ) ) ;
#17942=CARTESIAN_POINT ( 'NONE',  ( 8.000000000000000000, -6.085920226791118992, 15.78165944574518775 ) ) ;
#17949=VECTOR ( 'NONE', #32312, 1000.000000000000000 ) ;
#17975=CIRCLE ( 'NONE', #11656, 3.999999999999996447 ) ;
#17980=ORIENTED_EDGE ( 'NONE', *, *, #27077, .F. ) ;
#17984=CIRCLE ( 'NONE', #11097, 19.99999999999998579 ) ;
#17985=CARTESIAN_POINT ( 'NONE',  ( 0.000000000000000000, -0.5097555531871997836, -19.99350267651955804 ) ) ;
#17991=DIRECTION ( 'NONE',  ( -1.000000000000000000, 0.000000000000000000, 0.000000000000000000 ) ) ;
#18017=CARTESIAN_POINT ( 'NONE',  ( 8.000000000000000000, 15.46619997295644389, -1.007799283846741556 ) ) ;
#18018=AXIS2_PLACEMENT_3D ( 'NONE', #20925, #12856, #23834 ) ;
#18027=ORIENTED_EDGE ( 'NONE', *, *, #18927, .T. ) ;
#18028=ORIENTED_EDGE ( 'NONE', *, *, #19643, .T. ) ;
#18058=ORIENTED_EDGE ( 'NONE', *, *, #23996, .F. ) ;
#18076=DIRECTION ( 'NONE',  ( 0.000000000000000000, 0.8660254037844398178, -0.4999999999999980016 ) ) ;
#18080=DIRECTION ( 'NONE',  ( 0.000000000000000000, -0.8660254037844329345, -0.5000000000000101030 ) ) ;
#18081=CARTESIAN_POINT ( 'NONE',  ( 8.000000000000000000, 17.06000345190455292, -10.43821259704003346 ) ) ;
#18089=CARTESIAN_POINT ( 'NONE',  ( 0.000000000000000000, 3.872983346207417021, -1.000000000000000000 ) ) ;
#18098=FILL_AREA_STYLE_COLOUR ( '', #19933 ) ;
#18121=DIRECTION ( 'NONE',  ( 0.000000000000000000, 0.000000000000000000, 1.000000000000000000 ) ) ;
#18128=CARTESIAN_POINT ( 'NONE',  ( 0.000000000000000000, 0.000000000000000000, 0.000000000000000000 ) ) ;
#18129=CIRCLE ( 'NONE', #33104, 7.199999999999992184 ) ;
#18132=CARTESIAN_POINT ( 'NONE',  ( 8.000000000000000000, -15.46619997295643856, 1.007799283846635863 ) ) ;
#18146=ORIENTED_EDGE ( 'NONE', *, *, #11236, .F. ) ;
#18147=VERTEX_POINT ( 'NONE', #33061 ) ;
#18154=CARTESIAN_POINT ( 'NONE',  ( 8.000000000000000000, 5.400000000000000355, -0.9999999999999985567 ) ) ;
#18155=VECTOR ( 'NONE', #23724, 1000.000000000000000 ) ;
#18162=CARTESIAN_POINT ( 'NONE',  ( 8.000000000000000000, 16.71027810728552154, 4.579731798933998732 ) ) ;
#18165=DIRECTION ( 'NONE',  ( -1.000000000000000000, 0.000000000000000000, 0.000000000000000000 ) ) ;
#18208=AXIS2_PLACEMENT_3D ( 'NONE', #33247, #19024, #27147 ) ;
#18220=CARTESIAN_POINT ( 'NONE',  ( 4.000000000000000000, -17.06000345190431844, -10.43821259704038695 ) ) ;
#18234=VECTOR ( 'NONE', #12986, 1000.000000000000000 ) ;
#18258=CARTESIAN_POINT ( 'NONE',  ( 8.000000000000000000, -0.3212489022564151142, -16.91141623315864706 ) ) ;
#18292=DIRECTION ( 'NONE',  ( 1.000000000000000000, 0.000000000000000000, 0.000000000000000000 ) ) ;
#18307=VECTOR ( 'NONE', #15218, 1000.000000000000000 ) ;
#18309=EDGE_CURVE ( 'NONE', #16212, #29334, #33268, .T. ) ;
#18358=DIRECTION ( 'NONE',  ( -1.000000000000000000, 0.000000000000000000, 0.000000000000000000 ) ) ;
#18374=VERTEX_POINT ( 'NONE', #7763 ) ;
#18377=CARTESIAN_POINT ( 'NONE',  ( 4.000000000000000000, -19.77827456857337651, 2.969824084036396528 ) ) ;
#18397=PLANE ( 'NONE',  #17359 ) ;
#18400=CARTESIAN_POINT ( 'NONE',  ( 4.000000000000000000, -7.317194182740272446, 18.61340026142649506 ) ) ;
#18405=DIRECTION ( 'NONE',  ( -1.000000000000000000, 0.000000000000000000, 0.000000000000000000 ) ) ;
#18435=AXIS2_PLACEMENT_3D ( 'NONE', #35151, #32257, #12993 ) ;
#18443=ADVANCED_FACE ( 'NONE', ( #24166 ), #35334, .T. ) ;
#18450=CARTESIAN_POINT ( 'NONE',  ( 4.000000000000000000, 7.317194182740155206, 18.61340026142654125 ) ) ;
#18458=VERTEX_POINT ( 'NONE', #16387 ) ;
#18483=CARTESIAN_POINT ( 'NONE',  ( 8.000000000000000000, 0.5097555531875970214, -19.99350267651952606 ) ) ;
#18487=EDGE_CURVE ( 'NONE', #24111, #13301, #10870, .T. ) ;
#18539=VERTEX_POINT ( 'NONE', #24869 ) ;
#18550=ORIENTED_EDGE ( 'NONE', *, *, #10455, .F. ) ;
#18566=CIRCLE ( 'NONE', #12243, 7.199999999999993072 ) ;
#18579=CARTESIAN_POINT ( 'NONE',  ( 8.000000000000000000, 5.482169781019050170, -16.00140663693117560 ) ) ;
#18603=( NAMED_UNIT ( * ) SI_UNIT ( $, .STERADIAN. ) SOLID_ANGLE_UNIT ( ) );
#18606=VERTEX_POINT ( 'NONE', #16912 ) ;
#18612=CIRCLE ( 'NONE', #11141, 19.99999999999998579 ) ;
#18619=AXIS2_PLACEMENT_3D ( 'NONE', #8754, #3207, #28047 ) ;
#18620=DIRECTION ( 'NONE',  ( -1.000000000000000000, 0.000000000000000000, 0.000000000000000000 ) ) ;
#18639=FACE_OUTER_BOUND ( 'NONE', #7255, .T. ) ;
#18641=DIRECTION ( 'NONE',  ( 1.000000000000000000, -0.000000000000000000, -0.000000000000000000 ) ) ;
#18657=CARTESIAN_POINT ( 'NONE',  ( 8.000000000000000000, 0.000000000000000000, 0.000000000000000000 ) ) ;
#18665=DIRECTION ( 'NONE',  ( 0.000000000000000000, 0.000000000000000000, -1.000000000000000000 ) ) ;
#18675=EDGE_CURVE ( 'NONE', #33313, #5508, #14398, .T. ) ;
#18681=CLOSED_SHELL ( 'NONE', ( #32588, #24946, #33552, #26659, #22063, #31566, #711, #3347, #1410, #32885, #25772, #10800, #3612, #31463, #9915, #15243, #14564, #31098, #10118, #12592, #29714, #21401, #19748, #32204, #28448, #34395, #35081, #2542, #28119, #25792, #29090, #27123, #7007, #1147, #19182, #23324, #31, #20657, #18443, #2125, #10605, #947, #22213, #2606, #15786, #19556, #15943, #28489, #31507, #10680, #19198, #25285, #10349, #20340, #14436, #9665, #22047, #34747, #20701, #26501, #5344, #2493, #26057, #22408, #11247, #16340, #23183, #217, #8209, #20979, #30045, #35058, #34107, #20461, #15330, #12916, #28299, #34355, #5980, #35448, #24035, #16681, #20443, #16754, #24315 ) ) ;
#18691=ORIENTED_EDGE ( 'NONE', *, *, #33966, .F. ) ;
#18696=ORIENTED_EDGE ( 'NONE', *, *, #1106, .F. ) ;
#18714=ORIENTED_EDGE ( 'NONE', *, *, #21547, .F. ) ;
#18717=ORIENTED_EDGE ( 'NONE', *, *, #13220, .F. ) ;
#18723=EDGE_CURVE ( 'NONE', #1299, #6291, #1090, .T. ) ;
#18733=EDGE_CURVE ( 'NONE', #33477, #11373, #35552, .T. ) ;
#18735=VERTEX_POINT ( 'NONE', #17985 ) ;
#18755=VERTEX_POINT ( 'NONE', #25937 ) ;
#18760=AXIS2_PLACEMENT_3D ( 'NONE', #723, #34405, #23222 ) ;
#18761=ORIENTED_EDGE ( 'NONE', *, *, #3107, .T. ) ;
#18772=AXIS2_PLACEMENT_3D ( 'NONE', #29048, #25996, #9608 ) ;
#18774=ORIENTED_EDGE ( 'NONE', *, *, #13960, .T. ) ;
#18782=ORIENTED_EDGE ( 'NONE', *, *, #33629, .F. ) ;
#18787=VECTOR ( 'NONE', #20774, 1000.000000000000000 ) ;
#18790=AXIS2_PLACEMENT_3D ( 'NONE', #8160, #21663, #10347 ) ;
#18815=CARTESIAN_POINT ( 'NONE',  ( 0.000000000000000000, 3.678165988948789877, -15.05623113391063406 ) ) ;
#18837=DIRECTION ( 'NONE',  ( -1.000000000000000000, 0.000000000000000000, 0.000000000000000000 ) ) ;
#18845=VECTOR ( 'NONE', #23762, 1000.000000000000000 ) ;
#18849=CARTESIAN_POINT ( 'NONE',  ( 8.000000000000000000, -11.11653975335798528, 12.74840161668727134 ) ) ;
#18853=DIRECTION ( 'NONE',  ( -1.000000000000000000, 0.000000000000000000, 0.000000000000000000 ) ) ;
#18859=DIRECTION ( 'NONE',  ( 0.000000000000000000, 0.000000000000000000, -1.000000000000000000 ) ) ;
#18860=ORIENTED_EDGE ( 'NONE', *, *, #5381, .F. ) ;
#18862=ORIENTED_EDGE ( 'NONE', *, *, #18927, .F. ) ;
#18885=CARTESIAN_POINT ( 'NONE',  ( 0.000000000000000000, 0.000000000000000000, 0.000000000000000000 ) ) ;
#18902=ORIENTED_EDGE ( 'NONE', *, *, #25520, .T. ) ;
#18927=EDGE_CURVE ( 'NONE', #21695, #21999, #10249, .T. ) ;
#18931=DIRECTION ( 'NONE',  ( -1.000000000000000000, 0.000000000000000000, 0.000000000000000000 ) ) ;
#18952=ORIENTED_EDGE ( 'NONE', *, *, #15178, .T. ) ;
#18958=( NAMED_UNIT ( * ) PLANE_ANGLE_UNIT ( ) SI_UNIT ( $, .RADIAN. ) );
#18960=ORIENTED_EDGE ( 'NONE', *, *, #26421, .F. ) ;
#18967=CARTESIAN_POINT ( 'NONE',  ( 0.000000000000000000, -15.46619997295641369, -1.007799283846847471 ) ) ;
#18992=CARTESIAN_POINT ( 'NONE',  ( 0.000000000000000000, 4.898587196589413815E-16, -4.000000000000000000 ) ) ;
#18993=FACE_OUTER_BOUND ( 'NONE', #35582, .T. ) ;
#18996=DIRECTION ( 'NONE',  ( -1.000000000000000000, 0.000000000000000000, 0.000000000000000000 ) ) ;
#19004=VECTOR ( 'NONE', #12028, 1000.000000000000000 ) ;
#19010=AXIS2_PLACEMENT_3D ( 'NONE', #21957, #2733, #21781 ) ;
#19016=EDGE_CURVE ( 'NONE', #26725, #11394, #1641, .T. ) ;
#19023=CARTESIAN_POINT ( 'NONE',  ( 8.000000000000000000, 12.49559743815781587, 9.169462670380628566 ) ) ;
#19024=DIRECTION ( 'NONE',  ( -1.000000000000000000, 0.000000000000000000, 0.000000000000000000 ) ) ;
#19025=DIRECTION ( 'NONE',  ( -1.000000000000000000, 0.000000000000000000, 0.000000000000000000 ) ) ;
#19048=EDGE_LOOP ( 'NONE', ( #4561, #17073, #7498, #3728 ) ) ;
#19054=DIRECTION ( 'NONE',  ( 1.000000000000000000, -0.000000000000000000, -0.000000000000000000 ) ) ;
#19062=DIRECTION ( 'NONE',  ( -1.000000000000000000, 0.000000000000000000, 0.000000000000000000 ) ) ;
#19075=CARTESIAN_POINT ( 'NONE',  ( 0.000000000000000000, 0.000000000000000000, 0.000000000000000000 ) ) ;
#19099=DIRECTION ( 'NONE',  ( 0.000000000000000000, 0.8660254037844365982, 0.5000000000000035527 ) ) ;
#19105=DIRECTION ( 'NONE',  ( -1.000000000000000000, 0.000000000000000000, 0.000000000000000000 ) ) ;
#19119=VERTEX_POINT ( 'NONE', #10016 ) ;
#19153=CARTESIAN_POINT ( 'NONE',  ( 4.000000000000000000, 17.56975900509189970, -9.555290079479078713 ) ) ;
#19170=ORIENTED_EDGE ( 'NONE', *, *, #8025, .T. ) ;
#19182=ADVANCED_FACE ( 'NONE', ( #27300 ), #32337, .T. ) ;
#19183=DIRECTION ( 'NONE',  ( -1.000000000000000000, 0.000000000000000000, 0.000000000000000000 ) ) ;
#19184=ORIENTED_EDGE ( 'NONE', *, *, #21404, .F. ) ;
#19195=CARTESIAN_POINT ( 'NONE',  ( 8.000000000000000000, -1.693188892523641798, -15.40623615209873876 ) ) ;
#19198=ADVANCED_FACE ( 'NONE', ( #22060 ), #33055, .T. ) ;
#19209=EDGE_CURVE ( 'NONE', #33313, #18606, #10278, .T. ) ;
#19212=DIRECTION ( 'NONE',  ( -1.000000000000000000, 0.000000000000000000, 0.000000000000000000 ) ) ;
#19214=CARTESIAN_POINT ( 'NONE',  ( 8.000000000000000000, 12.46108038583334299, -15.64357617738981787 ) ) ;
#19215=ORIENTED_EDGE ( 'NONE', *, *, #21239, .F. ) ;
#19269=CARTESIAN_POINT ( 'NONE',  ( 8.000000000000000000, 0.000000000000000000, 0.000000000000000000 ) ) ;
#19275=DIRECTION ( 'NONE',  ( -1.000000000000000000, 0.000000000000000000, 0.000000000000000000 ) ) ;
#19303=CARTESIAN_POINT ( 'NONE',  ( 0.000000000000000000, 10.62435788049461571, -13.16139124467909483 ) ) ;
#19307=CIRCLE ( 'NONE', #33680, 7.199999999999993960 ) ;
#19315=CARTESIAN_POINT ( 'NONE',  ( 8.000000000000000000, -14.18878633068154826, -6.236773481718229206 ) ) ;
#19332=LINE ( 'NONE', #30512, #26893 ) ;
#19362=DIRECTION ( 'NONE',  ( 0.000000000000000000, 0.000000000000000000, 1.000000000000000000 ) ) ;
#19370=AXIS2_PLACEMENT_3D ( 'NONE', #4483, #35080, #7338 ) ;
#19375=DIRECTION ( 'NONE',  ( -1.000000000000000000, 0.000000000000000000, 0.000000000000000000 ) ) ;
#19388=DIRECTION ( 'NONE',  ( 0.000000000000000000, 0.000000000000000000, 1.000000000000000000 ) ) ;
#19425=FACE_OUTER_BOUND ( 'NONE', #11086, .T. ) ;
#19441=DIRECTION ( 'NONE',  ( 0.000000000000000000, 0.000000000000000000, 1.000000000000000000 ) ) ;
#19481=ORIENTED_EDGE ( 'NONE', *, *, #24454, .T. ) ;
#19489=DIRECTION ( 'NONE',  ( 1.000000000000000000, -0.000000000000000000, 0.000000000000000000 ) ) ;
#19549=EDGE_LOOP ( 'NONE', ( #28652, #20839, #32017, #2114 ) ) ;
#19551=DIRECTION ( 'NONE',  ( 0.000000000000000000, 0.000000000000000000, 1.000000000000000000 ) ) ;
#19556=ADVANCED_FACE ( 'NONE', ( #28583 ), #29299, .T. ) ;
#19567=ORIENTED_EDGE ( 'NONE', *, *, #4481, .T. ) ;
#19590=VERTEX_POINT ( 'NONE', #34164 ) ;
#19603=DIRECTION ( 'NONE',  ( 0.000000000000000000, 0.000000000000000000, 1.000000000000000000 ) ) ;
#19607=EDGE_LOOP ( 'NONE', ( #22509, #33691, #7449, #15298 ) ) ;
#19620=CYLINDRICAL_SURFACE ( 'NONE', #23368, 15.49899999999998457 ) ;
#19643=EDGE_CURVE ( 'NONE', #9129, #11554, #20646, .T. ) ;
#19662=ORIENTED_EDGE ( 'NONE', *, *, #3532, .F. ) ;
#19669=DIRECTION ( 'NONE',  ( 0.000000000000000000, 0.000000000000000000, -1.000000000000000000 ) ) ;
#19670=EDGE_CURVE ( 'NONE', #2896, #19816, #9750, .T. ) ;
#19676=DIRECTION ( 'NONE',  ( -1.000000000000000000, 0.000000000000000000, 0.000000000000000000 ) ) ;
#19702=AXIS2_PLACEMENT_3D ( 'NONE', #20496, #1621, #7541 ) ;
#19703=CIRCLE ( 'NONE', #765, 19.99999999999998579 ) ;
#19708=DIRECTION ( 'NONE',  ( -1.000000000000000000, 0.000000000000000000, 0.000000000000000000 ) ) ;
#19727=FACE_OUTER_BOUND ( 'NONE', #12482, .T. ) ;
#19747=DIRECTION ( 'NONE',  ( 0.000000000000000000, -6.983129352544641692E-15, 1.000000000000000000 ) ) ;
#19748=ADVANCED_FACE ( 'NONE', ( #109 ), #21891, .T. ) ;
#19752=VERTEX_POINT ( 'NONE', #8207 ) ;
#19805=EDGE_CURVE ( 'NONE', #9366, #10551, #13208, .T. ) ;
#19807=ORIENTED_EDGE ( 'NONE', *, *, #20217, .F. ) ;
#19810=ORIENTED_EDGE ( 'NONE', *, *, #1981, .T. ) ;
#19812=CARTESIAN_POINT ( 'NONE',  ( 8.000000000000000000, 0.000000000000000000, 0.000000000000000000 ) ) ;
#19816=VERTEX_POINT ( 'NONE', #11784 ) ;
#19818=DIRECTION ( 'NONE',  ( -1.000000000000000000, 0.000000000000000000, 0.000000000000000000 ) ) ;
#19819=PRODUCT_DEFINITION_SHAPE ( 'NONE', 'NONE',  #34383 ) ;
#19846=CARTESIAN_POINT ( 'NONE',  ( 0.000000000000000000, 16.71027810728552154, -2.620268201066000113 ) ) ;
#19859=ORIENTED_EDGE ( 'NONE', *, *, #30824, .F. ) ;
#19902=AXIS2_PLACEMENT_3D ( 'NONE', #5189, #16488, #5530 ) ;
#19916=DIRECTION ( 'NONE',  ( 0.000000000000000000, 0.000000000000000000, 1.000000000000000000 ) ) ;
#19925=FACE_OUTER_BOUND ( 'NONE', #29551, .T. ) ;
#19933=COLOUR_RGB ( '', 0.31764706, 0.68627451, 0.89019608) ;
#19936=DIRECTION ( 'NONE',  ( -1.000000000000000000, 0.000000000000000000, 0.000000000000000000 ) ) ;
#19946=ORIENTED_EDGE ( 'NONE', *, *, #8852, .F. ) ;
#19953=ORIENTED_EDGE ( 'NONE', *, *, #19209, .F. ) ;
#19992=ORIENTED_EDGE ( 'NONE', *, *, #23566, .T. ) ;
#19998=ORIENTED_EDGE ( 'NONE', *, *, #12303, .F. ) ;
#20008=CIRCLE ( 'NONE', #10257, 7.199999999999994849 ) ;
#20010=CARTESIAN_POINT ( 'NONE',  ( 50.00005079999999680, 5.400000000000000355, 0.9999999999999985567 ) ) ;
#20017=CARTESIAN_POINT ( 'NONE',  ( 0.000000000000000000, 17.56975900509189970, -9.555290079479078713 ) ) ;
#20033=VERTEX_POINT ( 'NONE', #31589 ) ;
#20039=ORIENTED_EDGE ( 'NONE', *, *, #25810, .T. ) ;
#20051=CARTESIAN_POINT ( 'NONE',  ( 0.000000000000000000, 0.000000000000000000, 0.000000000000000000 ) ) ;
#20066=DIRECTION ( 'NONE',  ( 0.000000000000000000, 0.000000000000000000, 1.000000000000000000 ) ) ;
#20077=FACE_OUTER_BOUND ( 'NONE', #17818, .T. ) ;
#20111=VERTEX_POINT ( 'NONE', #28537 ) ;
#20134=ORIENTED_EDGE ( 'NONE', *, *, #15343, .F. ) ;
#20137=CARTESIAN_POINT ( 'NONE',  ( 8.000000000000000000, 16.59870953437680896, 3.253005020243904255 ) ) ;
#20139=EDGE_LOOP ( 'NONE', ( #27027, #31536, #7887, #17525 ) ) ;
#20165=EDGE_LOOP ( 'NONE', ( #3348, #26602, #7394, #28116 ) ) ;
#20168=LINE ( 'NONE', #31174, #23990 ) ;
#20171=ORIENTED_EDGE ( 'NONE', *, *, #22026, .T. ) ;
#20181=CARTESIAN_POINT ( 'NONE',  ( 0.000000000000000000, -14.87816164169111133, -4.342730381190020417 ) ) ;
#20192=CARTESIAN_POINT ( 'NONE',  ( 8.000000000000000000, -10.62435788049434038, -13.16139124467930444 ) ) ;
#20208=DIRECTION ( 'NONE',  ( -1.000000000000000000, 0.000000000000000000, 0.000000000000000000 ) ) ;
#20212=EDGE_CURVE ( 'NONE', #18458, #4062, #21304, .T. ) ;
#20216=AXIS2_PLACEMENT_3D ( 'NONE', #21513, #35408, #34882 ) ;
#20217=EDGE_CURVE ( 'NONE', #1101, #5612, #1736, .T. ) ;
#20246=EDGE_CURVE ( 'NONE', #15919, #20473, #17229, .T. ) ;
#20284=DIRECTION ( 'NONE',  ( -1.000000000000000000, 0.000000000000000000, 0.000000000000000000 ) ) ;
#20288=VERTEX_POINT ( 'NONE', #8865 ) ;
#20290=AXIS2_PLACEMENT_3D ( 'NONE', #27653, #444, #2992 ) ;
#20296=ORIENTED_EDGE ( 'NONE', *, *, #28596, .F. ) ;
#20297=DIRECTION ( 'NONE',  ( -1.000000000000000000, 0.000000000000000000, 0.000000000000000000 ) ) ;
#20313=CARTESIAN_POINT ( 'NONE',  ( 0.000000000000000000, -7.317194182740013098, -18.61340026142654480 ) ) ;
#20333=ORIENTED_EDGE ( 'NONE', *, *, #18309, .F. ) ;
#20340=ADVANCED_FACE ( 'NONE', ( #11745 ), #2797, .T. ) ;
#20341=ORIENTED_EDGE ( 'NONE', *, *, #5842, .F. ) ;
#20347=DIRECTION ( 'NONE',  ( -1.000000000000000000, 0.000000000000000000, 0.000000000000000000 ) ) ;
#20353=ORIENTED_EDGE ( 'NONE', *, *, #35297, .T. ) ;
#20365=UNCERTAINTY_MEASURE_WITH_UNIT (LENGTH_MEASURE( 1.000000000000000082E-05 ), #10687, 'distance_accuracy_value', 'NONE');
#20367=DIRECTION ( 'NONE',  ( 0.000000000000000000, 0.3420201433256629397, 0.9396926207859104263 ) ) ;
#20371=LINE ( 'NONE', #34089, #27221 ) ;
#20372=ORIENTED_EDGE ( 'NONE', *, *, #28839, .T. ) ;
#20373=DIRECTION ( 'NONE',  ( 1.000000000000000000, -0.000000000000000000, -0.000000000000000000 ) ) ;
#20388=CIRCLE ( 'NONE', #11220, 19.99999999999998579 ) ;
#20393=CIRCLE ( 'NONE', #5474, 7.199999999999991296 ) ;
#20407=ORIENTED_EDGE ( 'NONE', *, *, #21430, .T. ) ;
#20423=ORIENTED_EDGE ( 'NONE', *, *, #1106, .T. ) ;
#20443=ADVANCED_FACE ( 'NONE', ( #25449 ), #9051, .T. ) ;
#20456=DIRECTION ( 'NONE',  ( 1.000000000000000000, -0.000000000000000000, -0.000000000000000000 ) ) ;
#20458=EDGE_CURVE ( 'NONE', #21073, #8899, #10069, .T. ) ;
#20461=ADVANCED_FACE ( 'NONE', ( #7715 ), #7378, .T. ) ;
#20465=VECTOR ( 'NONE', #5539, 1000.000000000000000 ) ;
#20469=AXIS2_PLACEMENT_3D ( 'NONE', #5271, #19105, #30102 ) ;
#20473=VERTEX_POINT ( 'NONE', #29174 ) ;
#20489=VECTOR ( 'NONE', #26749, 1000.000000000000000 ) ;
#20496=CARTESIAN_POINT ( 'NONE',  ( 8.000000000000000000, 0.000000000000000000, 0.000000000000000000 ) ) ;
#20513=EDGE_CURVE ( 'NONE', #12757, #8637, #26498, .T. ) ;
#20525=DIRECTION ( 'NONE',  ( -1.000000000000000000, 0.000000000000000000, 0.000000000000000000 ) ) ;
#20538=EDGE_LOOP ( 'NONE', ( #1607, #6768, #13183, #17223 ) ) ;
#20539=EDGE_CURVE ( 'NONE', #4854, #3615, #33388, .T. ) ;
#20601=CARTESIAN_POINT ( 'NONE',  ( 8.000000000000000000, -14.80634052301628145, 8.177498406287162069 ) ) ;
#20606=DIRECTION ( 'NONE',  ( -1.000000000000000000, 0.000000000000000000, 0.000000000000000000 ) ) ;
#20614=SURFACE_STYLE_USAGE ( .BOTH. , #29101 ) ;
#20646=CIRCLE ( 'NONE', #11469, 19.99999999999998579 ) ;
#20657=ADVANCED_FACE ( 'NONE', ( #3939 ), #30575, .T. ) ;
#20659=AXIS2_PLACEMENT_3D ( 'NONE', #11024, #21987, #29761 ) ;
#20661=ORIENTED_EDGE ( 'NONE', *, *, #13922, .F. ) ;
#20693=CARTESIAN_POINT ( 'NONE',  ( 8.000000000000000000, 0.000000000000000000, 0.000000000000000000 ) ) ;
#20701=ADVANCED_FACE ( 'NONE', ( #10029 ), #10218, .T. ) ;
#20723=LINE ( 'NONE', #14800, #7439 ) ;
#20732=LINE ( 'NONE', #18220, #15805 ) ;
#20744=DIRECTION ( 'NONE',  ( 0.000000000000000000, 0.6427876096865349220, 0.7660444431189816772 ) ) ;
#20756=ORIENTED_EDGE ( 'NONE', *, *, #7459, .T. ) ;
#20774=DIRECTION ( 'NONE',  ( -1.000000000000000000, 0.000000000000000000, 0.000000000000000000 ) ) ;
#20776=ORIENTED_EDGE ( 'NONE', *, *, #34662, .T. ) ;
#20777=CARTESIAN_POINT ( 'NONE',  ( 8.000000000000000000, -14.48509162075970202, 8.733917826871310908 ) ) ;
#20791=ORIENTED_EDGE ( 'NONE', *, *, #3623, .F. ) ;
#20797=CARTESIAN_POINT ( 'NONE',  ( 8.000000000000000000, -16.59870953437682672, 3.253005020243791456 ) ) ;
#20811=CYLINDRICAL_SURFACE ( 'NONE', #22070, 7.199999999999994849 ) ;
#20815=DIRECTION ( 'NONE',  ( 0.000000000000000000, 0.000000000000000000, -1.000000000000000000 ) ) ;
#20827=ORIENTED_EDGE ( 'NONE', *, *, #25398, .F. ) ;
#20839=ORIENTED_EDGE ( 'NONE', *, *, #22912, .T. ) ;
#20853=EDGE_CURVE ( 'NONE', #19816, #7160, #32860, .T. ) ;
#20870=ORIENTED_EDGE ( 'NONE', *, *, #14319, .T. ) ;
#20874=AXIS2_PLACEMENT_3D ( 'NONE', #2082, #32306, #4953 ) ;
#20883=EDGE_LOOP ( 'NONE', ( #1795, #22750, #15290, #12495 ) ) ;
#20894=EDGE_LOOP ( 'NONE', ( #5802, #14819, #31444, #12542 ) ) ;
#20895=VERTEX_POINT ( 'NONE', #16659 ) ;
#20908=AXIS2_PLACEMENT_3D ( 'NONE', #21715, #5700, #10930 ) ;
#20919=DIRECTION ( 'NONE',  ( 0.000000000000000000, 0.000000000000000000, -1.000000000000000000 ) ) ;
#20923=CARTESIAN_POINT ( 'NONE',  ( 0.000000000000000000, 0.000000000000000000, 0.000000000000000000 ) ) ;
#20925=CARTESIAN_POINT ( 'NONE',  ( 8.000000000000000000, 0.000000000000000000, 0.000000000000000000 ) ) ;
#20932=ORIENTED_EDGE ( 'NONE', *, *, #7540, .F. ) ;
#20949=ORIENTED_EDGE ( 'NONE', *, *, #21330, .F. ) ;
#20960=LINE ( 'NONE', #10535, #4456 ) ;
#20965=CARTESIAN_POINT ( 'NONE',  ( 0.000000000000000000, 15.46619997295644389, -1.007799283846741334 ) ) ;
#20967=ORIENTED_EDGE ( 'NONE', *, *, #1620, .F. ) ;
#20979=ADVANCED_FACE ( 'NONE', ( #27309 ), #21894, .T. ) ;
#20985=AXIS2_PLACEMENT_3D ( 'NONE', #28736, #3902, #4088 ) ;
#20988=EDGE_CURVE ( 'NONE', #4405, #10551, #32887, .T. ) ;
#20996=CARTESIAN_POINT ( 'NONE',  ( 8.000000000000000000, 0.3212489022565391261, 16.91141623315867193 ) ) ;
#21018=ORIENTED_EDGE ( 'NONE', *, *, #30365, .T. ) ;
#21032=ORIENTED_EDGE ( 'NONE', *, *, #12599, .F. ) ;
#21033=CARTESIAN_POINT ( 'NONE',  ( 8.000000000000000000, 6.359167119270465740, 18.96209359615096091 ) ) ;
#21034=DIRECTION ( 'NONE',  ( -1.000000000000000000, 0.000000000000000000, 0.000000000000000000 ) ) ;
#21058=ORIENTED_EDGE ( 'NONE', *, *, #13070, .T. ) ;
#21073=VERTEX_POINT ( 'NONE', #11270 ) ;
#21078=ORIENTED_EDGE ( 'NONE', *, *, #23996, .T. ) ;
#21105=VECTOR ( 'NONE', #16189, 1000.000000000000000 ) ;
#21133=DIRECTION ( 'NONE',  ( 0.000000000000000000, 0.000000000000000000, 1.000000000000000000 ) ) ;
#21152=AXIS2_PLACEMENT_3D ( 'NONE', #23036, #3982, #1439 ) ;
#21156=AXIS2_PLACEMENT_3D ( 'NONE', #23930, #32027, #23743 ) ;
#21160=AXIS2_PLACEMENT_3D ( 'NONE', #537, #11517, #22489 ) ;
#21164=CARTESIAN_POINT ( 'NONE',  ( 8.000000000000000000, 12.49559743815794199, -9.169462670380459812 ) ) ;
#21190=EDGE_CURVE ( 'NONE', #10377, #27557, #23723, .T. ) ;
#21193=DIRECTION ( 'NONE',  ( 1.000000000000000000, -0.000000000000000000, -0.000000000000000000 ) ) ;
#21196=FACE_OUTER_BOUND ( 'NONE', #22281, .T. ) ;
#21239=EDGE_CURVE ( 'NONE', #27661, #9040, #17975, .T. ) ;
#21245=DIRECTION ( 'NONE',  ( 0.000000000000000000, 0.000000000000000000, 1.000000000000000000 ) ) ;
#21251=CARTESIAN_POINT ( 'NONE',  ( 50.00005079999999680, 4.898587196589408884E-16, -3.999999999999996447 ) ) ;
#21275=ORIENTED_EDGE ( 'NONE', *, *, #16477, .T. ) ;
#21277=LINE ( 'NONE', #7771, #1038 ) ;
#21286=CIRCLE ( 'NONE', #598, 7.200000000000000178 ) ;
#21295=SURFACE_STYLE_FILL_AREA ( #13040 ) ;
#21304=LINE ( 'NONE', #32837, #10378 ) ;
#21307=AXIS2_PLACEMENT_3D ( 'NONE', #26589, #12725, #18292 ) ;
#21318=CARTESIAN_POINT ( 'NONE',  ( 4.000000000000000000, -6.359167119270330737, -18.96209359615098577 ) ) ;
#21324=DIRECTION ( 'NONE',  ( 1.000000000000000000, -0.000000000000000000, -0.000000000000000000 ) ) ;
#21325=DIRECTION ( 'NONE',  ( 0.000000000000000000, 0.3420201433256629397, 0.9396926207859104263 ) ) ;
#21330=EDGE_CURVE ( 'NONE', #18539, #28345, #22020, .T. ) ;
#21331=VERTEX_POINT ( 'NONE', #10167 ) ;
#21340=COLOUR_RGB ( '', 0.31764706, 0.68627451, 0.89019608) ;
#21366=DIRECTION ( 'NONE',  ( 0.000000000000000000, -0.8660254037844327124, -0.5000000000000101030 ) ) ;
#21369=ORIENTED_EDGE ( 'NONE', *, *, #13960, .F. ) ;
#21370=EDGE_CURVE ( 'NONE', #8637, #31804, #29522, .T. ) ;
#21378=DIRECTION ( 'NONE',  ( -1.000000000000000000, 0.000000000000000000, 0.000000000000000000 ) ) ;
#21381=ORIENTED_EDGE ( 'NONE', *, *, #4066, .F. ) ;
#21385=CIRCLE ( 'NONE', #20216, 7.199999999999994849 ) ;
#21388=CARTESIAN_POINT ( 'NONE',  ( 0.000000000000000000, 6.359167119270465740, 18.96209359615096446 ) ) ;
#21401=ADVANCED_FACE ( 'NONE', ( #72 ), #35032, .T. ) ;
#21404=EDGE_CURVE ( 'NONE', #14060, #32241, #19703, .T. ) ;
#21409=VERTEX_POINT ( 'NONE', #29437 ) ;
#21424=AXIS2_PLACEMENT_3D ( 'NONE', #24176, #32449, #16042 ) ;
#21430=EDGE_CURVE ( 'NONE', #6464, #27557, #8799, .T. ) ;
#21448=DIRECTION ( 'NONE',  ( -1.000000000000000000, 0.000000000000000000, 0.000000000000000000 ) ) ;
#21450=EDGE_LOOP ( 'NONE', ( #33134, #30049, #24405, #10126 ) ) ;
#21451=FACE_OUTER_BOUND ( 'NONE', #35457, .T. ) ;
#21457=VECTOR ( 'NONE', #1810, 1000.000000000000000 ) ;
#21494=LINE ( 'NONE', #17913, #6155 ) ;
#21501=CYLINDRICAL_SURFACE ( 'NONE', #2689, 19.99999999999998579 ) ;
#21513=CARTESIAN_POINT ( 'NONE',  ( 0.000000000000000000, -5.482169781018935595, 16.00140663693123599 ) ) ;
#21515=ORIENTED_EDGE ( 'NONE', *, *, #13937, .T. ) ;
#21545=ORIENTED_EDGE ( 'NONE', *, *, #9065, .F. ) ;
#21547=EDGE_CURVE ( 'NONE', #33707, #13869, #3100, .T. ) ;
#21560=DIRECTION ( 'NONE',  ( -1.000000000000000000, 0.000000000000000000, 0.000000000000000000 ) ) ;
#21562=FACE_OUTER_BOUND ( 'NONE', #1963, .T. ) ;
#21574=CYLINDRICAL_SURFACE ( 'NONE', #21851, 19.99999999999998579 ) ;
#21575=CARTESIAN_POINT ( 'NONE',  ( 8.000000000000000000, 0.000000000000000000, 0.000000000000000000 ) ) ;
#21593=VERTEX_POINT ( 'NONE', #11940 ) ;
#21616=CARTESIAN_POINT ( 'NONE',  ( 8.000000000000000000, 0.000000000000000000, 0.000000000000000000 ) ) ;
#21654=VERTEX_POINT ( 'NONE', #22728 ) ;
#21663=DIRECTION ( 'NONE',  ( -1.000000000000000000, 0.000000000000000000, 0.000000000000000000 ) ) ;
#21666=AXIS2_PLACEMENT_3D ( 'NONE', #10365, #28910, #26940 ) ;
#21686=CARTESIAN_POINT ( 'NONE',  ( 0.000000000000000000, -3.678165988948685516, 15.05623113391066070 ) ) ;
#21695=VERTEX_POINT ( 'NONE', #20017 ) ;
#21701=ORIENTED_EDGE ( 'NONE', *, *, #22026, .F. ) ;
#21705=CARTESIAN_POINT ( 'NONE',  ( 0.000000000000000000, 0.000000000000000000, 0.000000000000000000 ) ) ;
#21707=ORIENTED_EDGE ( 'NONE', *, *, #35246, .F. ) ;
#21715=CARTESIAN_POINT ( 'NONE',  ( 0.000000000000000000, -5.482169781018729537, -16.00140663693126086 ) ) ;
#21721=DIRECTION ( 'NONE',  ( 0.000000000000000000, -0.9848077530122097967, 0.1736481776669208388 ) ) ;
#21730=CARTESIAN_POINT ( 'NONE',  ( 8.000000000000000000, -6.860320204751237938, 13.89802171851381551 ) ) ;
#21743=VERTEX_POINT ( 'NONE', #33368 ) ;
#21748=VERTEX_POINT ( 'NONE', #16620 ) ;
#21761=CARTESIAN_POINT ( 'NONE',  ( 8.000000000000000000, 16.59870953437685515, -3.253005020243678214 ) ) ;
#21775=DIRECTION ( 'NONE',  ( -1.000000000000000000, 0.000000000000000000, 0.000000000000000000 ) ) ;
#21781=DIRECTION ( 'NONE',  ( 0.000000000000000000, 0.000000000000000000, 1.000000000000000000 ) ) ;
#21783=EDGE_LOOP ( 'NONE', ( #6117, #1454, #27738, #9300 ) ) ;
#21793=ORIENTED_EDGE ( 'NONE', *, *, #11387, .T. ) ;
#21805=CARTESIAN_POINT ( 'NONE',  ( 0.000000000000000000, 17.06000345190455647, -10.43821259704003523 ) ) ;
#21851=AXIS2_PLACEMENT_3D ( 'NONE', #7386, #17991, #26482 ) ;
#21883=DIRECTION ( 'NONE',  ( 0.000000000000000000, 0.000000000000000000, 1.000000000000000000 ) ) ;
#21891=CYLINDRICAL_SURFACE ( 'NONE', #13765, 19.99999999999998579 ) ;
#21894=CYLINDRICAL_SURFACE ( 'NONE', #12837, 15.49899999999998457 ) ;
#21902=DIRECTION ( 'NONE',  ( 0.000000000000000000, 0.000000000000000000, 1.000000000000000000 ) ) ;
#21908=AXIS2_PLACEMENT_3D ( 'NONE', #11307, #27530, #16516 ) ;
#21919=CARTESIAN_POINT ( 'NONE',  ( 0.000000000000000000, 0.3212489022565391261, 16.91141623315867193 ) ) ;
#21922=FACE_OUTER_BOUND ( 'NONE', #7996, .T. ) ;
#21939=LINE ( 'NONE', #30061, #8053 ) ;
#21940=CARTESIAN_POINT ( 'NONE',  ( 8.000000000000000000, -7.317194182740271557, 18.61340026142649151 ) ) ;
#21951=DIRECTION ( 'NONE',  ( 0.000000000000000000, 0.000000000000000000, 1.000000000000000000 ) ) ;
#21957=CARTESIAN_POINT ( 'NONE',  ( 8.000000000000000000, 14.48509162075963985, 8.733917826871412160 ) ) ;
#21959=ORIENTED_EDGE ( 'NONE', *, *, #14067, .T. ) ;
#21971=ORIENTED_EDGE ( 'NONE', *, *, #28893, .F. ) ;
#21974=CIRCLE ( 'NONE', #33490, 7.200000000000005507 ) ;
#21987=DIRECTION ( 'NONE',  ( -1.000000000000000000, 0.000000000000000000, 0.000000000000000000 ) ) ;
#21998=EDGE_CURVE ( 'NONE', #32241, #24079, #23952, .T. ) ;
#21999=VERTEX_POINT ( 'NONE', #21805 ) ;
#22008=DIRECTION ( 'NONE',  ( -1.000000000000000000, 0.000000000000000000, 0.000000000000000000 ) ) ;
#22010=ORIENTED_EDGE ( 'NONE', *, *, #35414, .T. ) ;
#22018=CYLINDRICAL_SURFACE ( 'NONE', #7050, 7.199999999999993960 ) ;
#22020=CIRCLE ( 'NONE', #25499, 7.199999999999992184 ) ;
#22026=EDGE_CURVE ( 'NONE', #22477, #31803, #10485, .T. ) ;
#22029=CARTESIAN_POINT ( 'NONE',  ( 8.000000000000000000, -17.56975900509186062, 9.555290079479195953 ) ) ;
#22030=VECTOR ( 'NONE', #13546, 1000.000000000000000 ) ;
#22047=ADVANCED_FACE ( 'NONE', ( #7423 ), #27231, .T. ) ;
#22060=FACE_OUTER_BOUND ( 'NONE', #7694, .T. ) ;
#22063=ADVANCED_FACE ( 'NONE', ( #7950 ), #5440, .T. ) ;
#22067=DIRECTION ( 'NONE',  ( -1.000000000000000000, 0.000000000000000000, 0.000000000000000000 ) ) ;
#22070=AXIS2_PLACEMENT_3D ( 'NONE', #20996, #15766, #26609 ) ;
#22081=ORIENTED_EDGE ( 'NONE', *, *, #15496, .T. ) ;
#22093=ORIENTED_EDGE ( 'NONE', *, *, #14550, .F. ) ;
#22124=ORIENTED_EDGE ( 'NONE', *, *, #30556, .T. ) ;
#22130=CARTESIAN_POINT ( 'NONE',  ( 8.000000000000000000, 12.49559743815781587, 9.169462670380628566 ) ) ;
#22162=FACE_OUTER_BOUND ( 'NONE', #29165, .T. ) ;
#22176=ORIENTED_EDGE ( 'NONE', *, *, #6885, .F. ) ;
#22179=EDGE_CURVE ( 'NONE', #10915, #20895, #25096, .T. ) ;
#22186=LINE ( 'NONE', #28311, #5099 ) ;
#22213=ADVANCED_FACE ( 'NONE', ( #8653 ), #19620, .T. ) ;
#22215=DIRECTION ( 'NONE',  ( 1.000000000000000000, -0.000000000000000000, -0.000000000000000000 ) ) ;
#22251=DIRECTION ( 'NONE',  ( 1.000000000000000000, -0.000000000000000000, 0.000000000000000000 ) ) ;
#22255=ORIENTED_EDGE ( 'NONE', *, *, #24145, .T. ) ;
#22273=CARTESIAN_POINT ( 'NONE',  ( 8.000000000000000000, -16.59870953437678409, -3.253005020244019718 ) ) ;
#22275=DIRECTION ( 'NONE',  ( 0.000000000000000000, 0.000000000000000000, 1.000000000000000000 ) ) ;
#22281=EDGE_LOOP ( 'NONE', ( #18058, #18862, #11161, #29956 ) ) ;
#22306=ORIENTED_EDGE ( 'NONE', *, *, #29084, .T. ) ;
#22350=CARTESIAN_POINT ( 'NONE',  ( 8.000000000000000000, -10.62435788049451624, 13.16139124467916588 ) ) ;
#22382=CARTESIAN_POINT ( 'NONE',  ( 8.000000000000000000, 11.19999565274265230, -10.71350075272062874 ) ) ;
#22394=DIRECTION ( 'NONE',  ( 0.000000000000000000, 0.000000000000000000, 1.000000000000000000 ) ) ;
#22408=ADVANCED_FACE ( 'NONE', ( #27192 ), #5054, .T. ) ;
#22422=DIRECTION ( 'NONE',  ( -1.000000000000000000, 0.000000000000000000, 0.000000000000000000 ) ) ;
#22428=LINE ( 'NONE', #22600, #20465 ) ;
#22432=ORIENTED_EDGE ( 'NONE', *, *, #33440, .F. ) ;
#22477=VERTEX_POINT ( 'NONE', #21940 ) ;
#22489=DIRECTION ( 'NONE',  ( 0.000000000000000000, -0.9848077530122063550, -0.1736481776669404342 ) ) ;
#22507=DIRECTION ( 'NONE',  ( -1.000000000000000000, 0.000000000000000000, 0.000000000000000000 ) ) ;
#22509=ORIENTED_EDGE ( 'NONE', *, *, #17193, .T. ) ;
#22511=AXIS2_PLACEMENT_3D ( 'NONE', #8472, #33143, #27046 ) ;
#22522=ORIENTED_EDGE ( 'NONE', *, *, #5182, .T. ) ;
#22540=AXIS2_PLACEMENT_3D ( 'NONE', #30532, #14129, #5514 ) ;
#22557=DIRECTION ( 'NONE',  ( 0.000000000000000000, -0.3420201433256758738, 0.9396926207859057634 ) ) ;
#22563=DIRECTION ( 'NONE',  ( 1.000000000000000000, -0.000000000000000000, -0.000000000000000000 ) ) ;
#22565=EDGE_LOOP ( 'NONE', ( #27492, #31926, #27429, #7020 ) ) ;
#22566=EDGE_CURVE ( 'NONE', #31574, #13189, #30584, .T. ) ;
#22597=VERTEX_POINT ( 'NONE', #15550 ) ;
#22600=CARTESIAN_POINT ( 'NONE',  ( 4.000000000000000000, -7.317194182740013098, -18.61340026142654480 ) ) ;
#22601=DIRECTION ( 'NONE',  ( 0.000000000000000000, 0.6427876096865403621, -0.7660444431189772363 ) ) ;
#22607=VECTOR ( 'NONE', #5571, 1000.000000000000000 ) ;
#22608=CARTESIAN_POINT ( 'NONE',  ( 8.000000000000000000, -0.5097555531874721213, 19.99350267651955093 ) ) ;
#22621=EDGE_LOOP ( 'NONE', ( #28966, #10985, #32784, #21018 ) ) ;
#22637=ORIENTED_EDGE ( 'NONE', *, *, #21330, .T. ) ;
#22686=CARTESIAN_POINT ( 'NONE',  ( 8.000000000000000000, 6.085920226791238008, -15.78165944574512203 ) ) ;
#22689=FACE_OUTER_BOUND ( 'NONE', #34330, .T. ) ;
#22705=EDGE_CURVE ( 'NONE', #12757, #2544, #10529, .T. ) ;
#22707=VERTEX_POINT ( 'NONE', #30150 ) ;
#22728=CARTESIAN_POINT ( 'NONE',  ( 0.000000000000000000, 12.46108038583314936, 15.64357617739001860 ) ) ;
#22736=DIRECTION ( 'NONE',  ( -1.000000000000000000, 0.000000000000000000, 0.000000000000000000 ) ) ;
#22738=CIRCLE ( 'NONE', #4371, 7.199999999999993072 ) ;
#22750=ORIENTED_EDGE ( 'NONE', *, *, #33674, .T. ) ;
#22764=AXIS2_PLACEMENT_3D ( 'NONE', #24100, #29665, #35086 ) ;
#22785=CARTESIAN_POINT ( 'NONE',  ( 8.000000000000000000, -17.06000345190431844, -10.43821259704038695 ) ) ;
#22827=CARTESIAN_POINT ( 'NONE',  ( 8.000000000000000000, 16.59870953437680896, 3.253005020243904255 ) ) ;
#22836=LINE ( 'NONE', #8974, #17692 ) ;
#22841=DIRECTION ( 'NONE',  ( 0.000000000000000000, 0.9848077530122085754, -0.1736481776669275556 ) ) ;
#22849=ORIENTED_EDGE ( 'NONE', *, *, #34662, .F. ) ;
#22876=EDGE_LOOP ( 'NONE', ( #5945, #2499, #34377, #27905 ) ) ;
#22912=EDGE_CURVE ( 'NONE', #32703, #24948, #29232, .T. ) ;
#22919=CARTESIAN_POINT ( 'NONE',  ( 8.000000000000000000, 5.400000000000000355, 0.9999999999999985567 ) ) ;
#22932=ORIENTED_EDGE ( 'NONE', *, *, #6928, .T. ) ;
#22939=CARTESIAN_POINT ( 'NONE',  ( 0.000000000000000000, 0.000000000000000000, 0.000000000000000000 ) ) ;
#22951=ORIENTED_EDGE ( 'NONE', *, *, #33966, .T. ) ;
#23026=AXIS2_PLACEMENT_3D ( 'NONE', #23721, #12570, #20815 ) ;
#23032=ORIENTED_EDGE ( 'NONE', *, *, #30246, .F. ) ;
#23036=CARTESIAN_POINT ( 'NONE',  ( 0.000000000000000000, 0.000000000000000000, 0.000000000000000000 ) ) ;
#23037=CARTESIAN_POINT ( 'NONE',  ( 0.000000000000000000, 0.000000000000000000, 20.00000000000000000 ) ) ;
#23049=DIRECTION ( 'NONE',  ( 0.000000000000000000, 0.000000000000000000, 1.000000000000000000 ) ) ;
#23055=DIRECTION ( 'NONE',  ( 0.000000000000000000, 0.000000000000000000, -1.000000000000000000 ) ) ;
#23086=CARTESIAN_POINT ( 'NONE',  ( 50.00005079999999680, 6.071532165918824830E-15, 1.000000000000000000 ) ) ;
#23089=DIRECTION ( 'NONE',  ( 0.000000000000000000, 0.000000000000000000, 1.000000000000000000 ) ) ;
#23095=CARTESIAN_POINT ( 'NONE',  ( 0.000000000000000000, 12.49559743815794199, -9.169462670380459812 ) ) ;
#23142=ORIENTED_EDGE ( 'NONE', *, *, #18723, .T. ) ;
#23151=DIRECTION ( 'NONE',  ( -1.000000000000000000, 0.000000000000000000, 0.000000000000000000 ) ) ;
#23156=VERTEX_POINT ( 'NONE', #10489 ) ;
#23160=DIRECTION ( 'NONE',  ( 1.000000000000000000, -0.000000000000000000, -0.000000000000000000 ) ) ;
#23166=CARTESIAN_POINT ( 'NONE',  ( 0.000000000000000000, -13.24207120356955159, -14.98824707027455183 ) ) ;
#23183=ADVANCED_FACE ( 'NONE', ( #7596 ), #16214, .T. ) ;
#23203=AXIS2_PLACEMENT_3D ( 'NONE', #13112, #6970, #27971 ) ;
#23204=DIRECTION ( 'NONE',  ( -1.000000000000000000, 0.000000000000000000, 0.000000000000000000 ) ) ;
#23213=DIRECTION ( 'NONE',  ( -1.000000000000000000, 0.000000000000000000, 0.000000000000000000 ) ) ;
#23216=VERTEX_POINT ( 'NONE', #4859 ) ;
#23222=DIRECTION ( 'NONE',  ( 0.000000000000000000, 0.000000000000000000, 1.000000000000000000 ) ) ;
#23234=DIRECTION ( 'NONE',  ( 0.000000000000000000, 0.000000000000000000, 1.000000000000000000 ) ) ;
#23240=CARTESIAN_POINT ( 'NONE',  ( 0.000000000000000000, -10.62435788049451624, 13.16139124467916588 ) ) ;
#23258=AXIS2_PLACEMENT_3D ( 'NONE', #28418, #9147, #14714 ) ;
#23264=DIRECTION ( 'NONE',  ( 0.000000000000000000, 0.000000000000000000, -1.000000000000000000 ) ) ;
#23270=CARTESIAN_POINT ( 'NONE',  ( 8.000000000000000000, -16.71027810728551799, 2.620268201065888203 ) ) ;
#23293=CARTESIAN_POINT ( 'NONE',  ( 0.000000000000000000, -16.71027810728550733, 4.579731798933884157 ) ) ;
#23306=CARTESIAN_POINT ( 'NONE',  ( 8.000000000000000000, -11.19999565274257414, 10.71350075272070512 ) ) ;
#23316=AXIS2_PLACEMENT_3D ( 'NONE', #16776, #14601, #30826 ) ;
#23324=ADVANCED_FACE ( 'NONE', ( #15623 ), #10258, .T. ) ;
#23329=CARTESIAN_POINT ( 'NONE',  ( 8.000000000000000000, -3.678165988948685516, 15.05623113391066070 ) ) ;
#23348=CIRCLE ( 'NONE', #25656, 15.49899999999998457 ) ;
#23354=EDGE_CURVE ( 'NONE', #10620, #28254, #4326, .T. ) ;
#23357=EDGE_CURVE ( 'NONE', #1299, #31574, #5935, .T. ) ;
#23368=AXIS2_PLACEMENT_3D ( 'NONE', #11541, #22507, #9006 ) ;
#23369=CARTESIAN_POINT ( 'NONE',  ( 8.000000000000000000, -3.678165988948487009, -15.05623113391071044 ) ) ;
#23373=ORIENTED_EDGE ( 'NONE', *, *, #31919, .T. ) ;
#23398=ORIENTED_EDGE ( 'NONE', *, *, #17035, .T. ) ;
#23415=ORIENTED_EDGE ( 'NONE', *, *, #30599, .F. ) ;
#23427=ORIENTED_EDGE ( 'NONE', *, *, #21998, .F. ) ;
#23437=CARTESIAN_POINT ( 'NONE',  ( 8.000000000000000000, -1.693188892523842082, 15.40623615209871566 ) ) ;
#23476=ORIENTED_EDGE ( 'NONE', *, *, #28853, .T. ) ;
#23509=LINE ( 'NONE', #34502, #32547 ) ;
#23518=DIRECTION ( 'NONE',  ( 0.000000000000000000, 0.6427876096865349220, 0.7660444431189816772 ) ) ;
#23523=CARTESIAN_POINT ( 'NONE',  ( 0.000000000000000000, -12.46108038583301791, -15.64357617739007722 ) ) ;
#23553=ORIENTED_EDGE ( 'NONE', *, *, #14324, .F. ) ;
#23562=EDGE_CURVE ( 'NONE', #33371, #19590, #31810, .T. ) ;
#23566=EDGE_CURVE ( 'NONE', #31804, #18147, #11109, .T. ) ;
#23570=ORIENTED_EDGE ( 'NONE', *, *, #28849, .F. ) ;
#23575=ORIENTED_EDGE ( 'NONE', *, *, #33158, .T. ) ;
#23582=CARTESIAN_POINT ( 'NONE',  ( -10.00000000000000000, 0.000000000000000000, 0.000000000000000000 ) ) ;
#23643=CARTESIAN_POINT ( 'NONE',  ( 50.00005079999999680, 0.000000000000000000, 0.000000000000000000 ) ) ;
#23651=DIRECTION ( 'NONE',  ( 1.000000000000000000, -0.000000000000000000, 0.000000000000000000 ) ) ;
#23658=ORIENTED_EDGE ( 'NONE', *, *, #27618, .T. ) ;
#23665=CIRCLE ( 'NONE', #9848, 15.49899999999997391 ) ;
#23673=DIRECTION ( 'NONE',  ( 0.000000000000000000, 0.000000000000000000, -1.000000000000000000 ) ) ;
#23675=ORIENTED_EDGE ( 'NONE', *, *, #13057, .T. ) ;
#23679=DIRECTION ( 'NONE',  ( 0.000000000000000000, 0.000000000000000000, -1.000000000000000000 ) ) ;
#23685=DIRECTION ( 'NONE',  ( -1.000000000000000000, 0.000000000000000000, 0.000000000000000000 ) ) ;
#23721=CARTESIAN_POINT ( 'NONE',  ( 0.000000000000000000, 6.085920226791021292, 15.78165944574522861 ) ) ;
#23723=CIRCLE ( 'NONE', #30638, 7.199999999999993960 ) ;
#23724=DIRECTION ( 'NONE',  ( -1.000000000000000000, 0.000000000000000000, 0.000000000000000000 ) ) ;
#23730=ORIENTED_EDGE ( 'NONE', *, *, #22912, .F. ) ;
#23743=DIRECTION ( 'NONE',  ( 0.000000000000000000, 0.000000000000000000, 1.000000000000000000 ) ) ;
#23752=AXIS2_PLACEMENT_3D ( 'NONE', #2198, #32584, #21245 ) ;
#23759=AXIS2_PLACEMENT_3D ( 'NONE', #29936, #29586, #7959 ) ;
#23762=DIRECTION ( 'NONE',  ( -1.000000000000000000, 0.000000000000000000, 0.000000000000000000 ) ) ;
#23771=CARTESIAN_POINT ( 'NONE',  ( 0.000000000000000000, -0.5097555531874712331, 19.99350267651955093 ) ) ;
#23779=DIRECTION ( 'NONE',  ( -1.000000000000000000, 0.000000000000000000, 0.000000000000000000 ) ) ;
#23824=EDGE_LOOP ( 'NONE', ( #21707, #8091, #28315, #4882 ) ) ;
#23834=DIRECTION ( 'NONE',  ( 0.000000000000000000, -0.3420201433256756518, 0.9396926207859058744 ) ) ;
#23878=EDGE_LOOP ( 'NONE', ( #696, #33179, #3120, #28523 ) ) ;
#23881=CARTESIAN_POINT ( 'NONE',  ( 8.000000000000000000, -0.3212489022566501484, 16.91141623315869680 ) ) ;
#23913=DIRECTION ( 'NONE',  ( 1.000000000000000000, -0.000000000000000000, 0.000000000000000000 ) ) ;
#23928=CIRCLE ( 'NONE', #8377, 15.49899999999998457 ) ;
#23930=CARTESIAN_POINT ( 'NONE',  ( 8.000000000000000000, 0.000000000000000000, 0.000000000000000000 ) ) ;
#23952=CIRCLE ( 'NONE', #2683, 7.199999999999993072 ) ;
#23959=ORIENTED_EDGE ( 'NONE', *, *, #7323, .T. ) ;
#23963=VECTOR ( 'NONE', #32822, 1000.000000000000000 ) ;
#23990=VECTOR ( 'NONE', #30994, 1000.000000000000000 ) ;
#23996=EDGE_CURVE ( 'NONE', #21999, #211, #9498, .T. ) ;
#24000=CIRCLE ( 'NONE', #14209, 15.49899999999998279 ) ;
#24004=CIRCLE ( 'NONE', #13084, 7.199999999999994849 ) ;
#24035=ADVANCED_FACE ( 'NONE', ( #15587 ), #20811, .T. ) ;
#24039=CIRCLE ( 'NONE', #10823, 19.99999999999998579 ) ;
#24060=CARTESIAN_POINT ( 'NONE',  ( 0.000000000000000000, -11.19999565274257414, 10.71350075272070512 ) ) ;
#24076=EDGE_CURVE ( 'NONE', #18374, #984, #15143, .T. ) ;
#24079=VERTEX_POINT ( 'NONE', #19315 ) ;
#24100=CARTESIAN_POINT ( 'NONE',  ( -10.00000000000000000, 0.000000000000000000, 0.000000000000000000 ) ) ;
#24107=EDGE_LOOP ( 'NONE', ( #26093, #7564, #1479, #2594, #31223, #20661, #13479, #19807, #20791, #10452, #19998, #18714, #13179, #32161, #9337, #14599, #12720, #985, #12033, #16283, #11250, #17310, #18717, #30067, #7223, #25017, #28956, #20932, #20333, #10460, #17085, #268, #6290, #23427, #19184, #21971, #23570, #23032, #6639, #29803, #16740, #25338, #4230, #16261, #24271, #29423, #33111, #2849, #5993, #25943, #30205, #22432, #12043, #7488, #32654, #18696, #27392, #11853, #12219, #18860, #19953, #8611, #12989, #15375, #1215, #26775, #17980, #21545, #7691, #27014, #4130, #7299, #20949, #17325, #24859, #32544, #32536 ) ) ;
#24111=VERTEX_POINT ( 'NONE', #22029 ) ;
#24135=DIRECTION ( 'NONE',  ( 0.000000000000000000, 0.000000000000000000, 1.000000000000000000 ) ) ;
#24145=EDGE_CURVE ( 'NONE', #28086, #26963, #30846, .T. ) ;
#24156=EDGE_LOOP ( 'NONE', ( #19, #9297, #6662, #1713 ) ) ;
#24166=FACE_OUTER_BOUND ( 'NONE', #22621, .T. ) ;
#24176=CARTESIAN_POINT ( 'NONE',  ( 8.000000000000000000, 0.000000000000000000, 0.000000000000000000 ) ) ;
#24177=LINE ( 'NONE', #2581, #22030 ) ;
#24179=CIRCLE ( 'NONE', #1741, 7.199999999999993072 ) ;
#24201=AXIS2_PLACEMENT_3D ( 'NONE', #3406, #14886, #19916 ) ;
#24217=CARTESIAN_POINT ( 'NONE',  ( 8.000000000000000000, -14.87816164169118416, 4.342730381189816136 ) ) ;
#24220=CARTESIAN_POINT ( 'NONE',  ( 0.000000000000000000, 0.000000000000000000, 0.000000000000000000 ) ) ;
#24225=DIRECTION ( 'NONE',  ( -1.000000000000000000, 0.000000000000000000, 0.000000000000000000 ) ) ;
#24268=DIRECTION ( 'NONE',  ( 1.000000000000000000, -0.000000000000000000, 0.000000000000000000 ) ) ;
#24271=ORIENTED_EDGE ( 'NONE', *, *, #31688, .F. ) ;
#24273=EDGE_CURVE ( 'NONE', #24979, #32647, #2021, .T. ) ;
#24285=DIRECTION ( 'NONE',  ( 0.000000000000000000, 0.8660254037844398178, -0.4999999999999981681 ) ) ;
#24295=CYLINDRICAL_SURFACE ( 'NONE', #29333, 3.999999999999996447 ) ;
#24315=ADVANCED_FACE ( 'NONE', ( #31378 ), #17862, .T. ) ;
#24345=FACE_BOUND ( 'NONE', #6510, .T. ) ;
#24350=AXIS2_PLACEMENT_3D ( 'NONE', #29617, #11059, #15726 ) ;
#24351=DIRECTION ( 'NONE',  ( -1.000000000000000000, 0.000000000000000000, 0.000000000000000000 ) ) ;
#24381=EDGE_CURVE ( 'NONE', #19752, #9468, #6037, .T. ) ;
#24400=DIRECTION ( 'NONE',  ( 1.000000000000000000, -0.000000000000000000, -0.000000000000000000 ) ) ;
#24405=ORIENTED_EDGE ( 'NONE', *, *, #3921, .T. ) ;
#24411=FACE_OUTER_BOUND ( 'NONE', #5449, .T. ) ;
#24414=ORIENTED_EDGE ( 'NONE', *, *, #32019, .T. ) ;
#24415=EDGE_CURVE ( 'NONE', #14060, #15919, #20732, .T. ) ;
#24454=EDGE_CURVE ( 'NONE', #17379, #31396, #29931, .T. ) ;
#24464=CIRCLE ( 'NONE', #29065, 7.199999999999994849 ) ;
#24470=ORIENTED_EDGE ( 'NONE', *, *, #24273, .F. ) ;
#24481=DIRECTION ( 'NONE',  ( 1.000000000000000000, -0.000000000000000000, -0.000000000000000000 ) ) ;
#24500=AXIS2_PLACEMENT_3D ( 'NONE', #8959, #11497, #3583 ) ;
#24501=FACE_OUTER_BOUND ( 'NONE', #15041, .T. ) ;
#24529=ORIENTED_EDGE ( 'NONE', *, *, #13286, .T. ) ;
#24560=DIRECTION ( 'NONE',  ( 0.000000000000000000, 0.000000000000000000, 1.000000000000000000 ) ) ;
#24564=DIRECTION ( 'NONE',  ( -1.000000000000000000, 0.000000000000000000, 0.000000000000000000 ) ) ;
#24578=VECTOR ( 'NONE', #2552, 1000.000000000000000 ) ;
#24580=CARTESIAN_POINT ( 'NONE',  ( 8.000000000000000000, 11.19999565274250308, 10.71350075272077973 ) ) ;
#24593=CIRCLE ( 'NONE', #26915, 7.199999999999993072 ) ;
#24601=ORIENTED_EDGE ( 'NONE', *, *, #15664, .F. ) ;
#24622=DIRECTION ( 'NONE',  ( -1.000000000000000000, 0.000000000000000000, 0.000000000000000000 ) ) ;
#24632=DIRECTION ( 'NONE',  ( 0.000000000000000000, -1.000000000000000000, 0.000000000000000000 ) ) ;
#24645=CIRCLE ( 'NONE', #9107, 7.199999999999992184 ) ;
#24653=LINE ( 'NONE', #14009, #22607 ) ;
#24664=ORIENTED_EDGE ( 'NONE', *, *, #274, .F. ) ;
#24671=CYLINDRICAL_SURFACE ( 'NONE', #8502, 7.199999999999994849 ) ;
#24713=EDGE_LOOP ( 'NONE', ( #17465, #27041, #5859, #15175 ) ) ;
#24715=CARTESIAN_POINT ( 'NONE',  ( 8.000000000000000000, -11.11653975335798528, 12.74840161668727134 ) ) ;
#24730=EDGE_CURVE ( 'NONE', #18755, #17047, #11228, .T. ) ;
#24756=DIRECTION ( 'NONE',  ( -1.000000000000000000, 0.000000000000000000, 0.000000000000000000 ) ) ;
#24764=CARTESIAN_POINT ( 'NONE',  ( 0.000000000000000000, 19.77827456857338007, -2.969824084036534639 ) ) ;
#24776=EDGE_LOOP ( 'NONE', ( #6818, #18550, #16278, #18952 ) ) ;
#24777=DIRECTION ( 'NONE',  ( 0.000000000000000000, 0.000000000000000000, 1.000000000000000000 ) ) ;
#24793=DIRECTION ( 'NONE',  ( 0.000000000000000000, 0.3420201433256629953, 0.9396926207859105373 ) ) ;
#24794=FACE_OUTER_BOUND ( 'NONE', #2455, .T. ) ;
#24801=AXIS2_PLACEMENT_3D ( 'NONE', #31316, #889, #28626 ) ;
#24802=DIRECTION ( 'NONE',  ( 0.000000000000000000, 0.000000000000000000, 1.000000000000000000 ) ) ;
#24835=DIRECTION ( 'NONE',  ( 0.000000000000000000, -0.6427876096865297040, -0.7660444431189861181 ) ) ;
#24850=CARTESIAN_POINT ( 'NONE',  ( 8.000000000000000000, 0.000000000000000000, 0.000000000000000000 ) ) ;
#24859=ORIENTED_EDGE ( 'NONE', *, *, #35459, .F. ) ;
#24869=CARTESIAN_POINT ( 'NONE',  ( 8.000000000000000000, 16.59870953437680896, 10.45300502024390354 ) ) ;
#24871=EDGE_CURVE ( 'NONE', #28086, #7873, #18129, .T. ) ;
#24889=DIRECTION ( 'NONE',  ( 0.000000000000000000, -0.6427876096865294819, -0.7660444431189861181 ) ) ;
#24913=DIRECTION ( 'NONE',  ( 0.000000000000000000, 0.000000000000000000, -1.000000000000000000 ) ) ;
#24921=AXIS2_PLACEMENT_3D ( 'NONE', #22686, #8491, #30468 ) ;
#24946=ADVANCED_FACE ( 'NONE', ( #34582 ), #12615, .T. ) ;
#24948=VERTEX_POINT ( 'NONE', #12791 ) ;
#24953=CIRCLE ( 'NONE', #20908, 7.199999999999992184 ) ;
#24967=CYLINDRICAL_SURFACE ( 'NONE', #26239, 19.99999999999998579 ) ;
#24979=VERTEX_POINT ( 'NONE', #29187 ) ;
#24987=FACE_OUTER_BOUND ( 'NONE', #27063, .T. ) ;
#24990=ORIENTED_EDGE ( 'NONE', *, *, #448, .T. ) ;
#25006=AXIS2_PLACEMENT_3D ( 'NONE', #23086, #23264, #29035 ) ;
#25012=CARTESIAN_POINT ( 'NONE',  ( 8.000000000000000000, 14.80634052301623171, -8.177498406287266874 ) ) ;
#25017=ORIENTED_EDGE ( 'NONE', *, *, #10653, .F. ) ;
#25025=VECTOR ( 'NONE', #23160, 1000.000000000000000 ) ;
#25042=AXIS2_PLACEMENT_3D ( 'NONE', #35214, #24400, #29089 ) ;
#25076=AXIS2_PLACEMENT_3D ( 'NONE', #823, #650, #127 ) ;
#25078=EDGE_CURVE ( 'NONE', #211, #10299, #27908, .T. ) ;
#25096=CIRCLE ( 'NONE', #11849, 15.49899999999999167 ) ;
#25099=CIRCLE ( 'NONE', #18772, 7.199999999999993072 ) ;
#25100=LINE ( 'NONE', #22382, #1312 ) ;
#25138=CARTESIAN_POINT ( 'NONE',  ( 0.000000000000000000, 14.80634052301623171, 8.177498406287277533 ) ) ;
#25174=CYLINDRICAL_SURFACE ( 'NONE', #15035, 3.999999999999996447 ) ;
#25233=AXIS2_PLACEMENT_3D ( 'NONE', #30133, #30315, #26919 ) ;
#25280=CARTESIAN_POINT ( 'NONE',  ( 0.000000000000000000, 16.71027810728552154, -2.620268201066000113 ) ) ;
#25285=ADVANCED_FACE ( 'NONE', ( #684 ), #11664, .T. ) ;
#25291=ORIENTED_EDGE ( 'NONE', *, *, #9286, .F. ) ;
#25294=FACE_OUTER_BOUND ( 'NONE', #25600, .T. ) ;
#25303=EDGE_CURVE ( 'NONE', #26998, #20111, #8947, .T. ) ;
#25304=DIRECTION ( 'NONE',  ( 0.000000000000000000, 0.9848077530122085754, -0.1736481776669275556 ) ) ;
#25338=ORIENTED_EDGE ( 'NONE', *, *, #21370, .F. ) ;
#25371=CYLINDRICAL_SURFACE ( 'NONE', #6920, 15.49899999999998457 ) ;
#25373=CARTESIAN_POINT ( 'NONE',  ( 0.000000000000000000, 0.000000000000000000, 0.000000000000000000 ) ) ;
#25389=LINE ( 'NONE', #17081, #34362 ) ;
#25398=EDGE_CURVE ( 'NONE', #932, #19590, #19307, .T. ) ;
#25430=FACE_OUTER_BOUND ( 'NONE', #21783, .T. ) ;
#25443=AXIS2_PLACEMENT_3D ( 'NONE', #14880, #28398, #12195 ) ;
#25449=FACE_OUTER_BOUND ( 'NONE', #33741, .T. ) ;
#25450=CARTESIAN_POINT ( 'NONE',  ( 0.000000000000000000, -17.06000345190446055, 10.43821259704015425 ) ) ;
#25472=ORIENTED_EDGE ( 'NONE', *, *, #10929, .T. ) ;
#25483=CARTESIAN_POINT ( 'NONE',  ( -10.00000000000000000, 0.000000000000000000, 0.000000000000000000 ) ) ;
#25489=DIRECTION ( 'NONE',  ( -1.000000000000000000, 0.000000000000000000, 0.000000000000000000 ) ) ;
#25499=AXIS2_PLACEMENT_3D ( 'NONE', #15366, #9634, #34485 ) ;
#25520=EDGE_CURVE ( 'NONE', #13855, #192, #13119, .T. ) ;
#25546=DIRECTION ( 'NONE',  ( 0.000000000000000000, 0.000000000000000000, 1.000000000000000000 ) ) ;
#25549=FACE_OUTER_BOUND ( 'NONE', #1754, .T. ) ;
#25563=CYLINDRICAL_SURFACE ( 'NONE', #17686, 19.99999999999998579 ) ;
#25588=CARTESIAN_POINT ( 'NONE',  ( 8.000000000000000000, 0.000000000000000000, 0.000000000000000000 ) ) ;
#25594=DIRECTION ( 'NONE',  ( -1.000000000000000000, 0.000000000000000000, 0.000000000000000000 ) ) ;
#25599=CARTESIAN_POINT ( 'NONE',  ( 0.000000000000000000, -19.77827456857337651, 2.969824084036395639 ) ) ;
#25600=EDGE_LOOP ( 'NONE', ( #21369, #13980, #5207, #16192 ) ) ;
#25613=CYLINDRICAL_SURFACE ( 'NONE', #9626, 7.199999999999994849 ) ;
#25639=EDGE_CURVE ( 'NONE', #17618, #23216, #2666, .T. ) ;
#25656=AXIS2_PLACEMENT_3D ( 'NONE', #20923, #3686, #25835 ) ;
#25663=LINE ( 'NONE', #9439, #32892 ) ;
#25669=AXIS2_PLACEMENT_3D ( 'NONE', #22827, #33825, #9149 ) ;
#25695=DIRECTION ( 'NONE',  ( -1.000000000000000000, 0.000000000000000000, 0.000000000000000000 ) ) ;
#25725=LINE ( 'NONE', #14712, #19004 ) ;
#25729=EDGE_CURVE ( 'NONE', #23216, #30129, #15890, .T. ) ;
#25740=LINE ( 'NONE', #8622, #16565 ) ;
#25743=EDGE_CURVE ( 'NONE', #26843, #12757, #3246, .T. ) ;
#25772=ADVANCED_FACE ( 'NONE', ( #24794 ), #24967, .T. ) ;
#25774=EDGE_CURVE ( 'NONE', #32593, #6961, #8978, .T. ) ;
#25780=CIRCLE ( 'NONE', #21156, 19.99999999999998579 ) ;
#25786=LINE ( 'NONE', #9022, #8690 ) ;
#25792=ADVANCED_FACE ( 'NONE', ( #28199 ), #33412, .T. ) ;
#25799=ORIENTED_EDGE ( 'NONE', *, *, #2527, .T. ) ;
#25810=EDGE_CURVE ( 'NONE', #31265, #27370, #17547, .T. ) ;
#25827=DIRECTION ( 'NONE',  ( -1.000000000000000000, 0.000000000000000000, 0.000000000000000000 ) ) ;
#25831=CARTESIAN_POINT ( 'NONE',  ( 8.000000000000000000, 0.000000000000000000, 0.000000000000000000 ) ) ;
#25835=DIRECTION ( 'NONE',  ( 0.000000000000000000, 0.000000000000000000, -1.000000000000000000 ) ) ;
#25843=EDGE_LOOP ( 'NONE', ( #2725, #2374, #2062, #17679 ) ) ;
#25866=CARTESIAN_POINT ( 'NONE',  ( 0.000000000000000000, 6.860320204751340079, -13.89802171851375689 ) ) ;
#25867=DIRECTION ( 'NONE',  ( -1.000000000000000000, 0.000000000000000000, 0.000000000000000000 ) ) ;
#25870=CARTESIAN_POINT ( 'NONE',  ( 0.000000000000000000, 0.000000000000000000, 0.000000000000000000 ) ) ;
#25871=EDGE_LOOP ( 'NONE', ( #7888, #10373, #31883, #19810 ) ) ;
#25910=AXIS2_PLACEMENT_3D ( 'NONE', #16369, #33132, #6110 ) ;
#25937=CARTESIAN_POINT ( 'NONE',  ( 8.000000000000000000, 6.860320204751148232, 13.89802171851385459 ) ) ;
#25941=FACE_OUTER_BOUND ( 'NONE', #9911, .T. ) ;
#25943=ORIENTED_EDGE ( 'NONE', *, *, #20853, .F. ) ;
#25956=CIRCLE ( 'NONE', #31112, 7.200000000000006395 ) ;
#25957=ORIENTED_EDGE ( 'NONE', *, *, #19016, .T. ) ;
#25992=CARTESIAN_POINT ( 'NONE',  ( 0.000000000000000000, 0.000000000000000000, 0.000000000000000000 ) ) ;
#25996=DIRECTION ( 'NONE',  ( -1.000000000000000000, 0.000000000000000000, 0.000000000000000000 ) ) ;
#26032=FACE_OUTER_BOUND ( 'NONE', #3874, .T. ) ;
#26041=EDGE_LOOP ( 'NONE', ( #16106, #22093, #29676, #1679 ) ) ;
#26052=AXIS2_PLACEMENT_3D ( 'NONE', #5669, #5146, #16086 ) ;
#26056=AXIS2_PLACEMENT_3D ( 'NONE', #16461, #33561, #22394 ) ;
#26057=ADVANCED_FACE ( 'NONE', ( #26032 ), #1542, .T. ) ;
#26059=VERTEX_POINT ( 'NONE', #29088 ) ;
#26091=ORIENTED_EDGE ( 'NONE', *, *, #21998, .T. ) ;
#26093=ORIENTED_EDGE ( 'NONE', *, *, #16752, .F. ) ;
#26105=CARTESIAN_POINT ( 'NONE',  ( 0.000000000000000000, -6.359167119270593638, 18.96209359615092183 ) ) ;
#26111=DIRECTION ( 'NONE',  ( -1.000000000000000000, 0.000000000000000000, 0.000000000000000000 ) ) ;
#26127=EDGE_CURVE ( 'NONE', #5642, #21593, #32141, .T. ) ;
#26134=CYLINDRICAL_SURFACE ( 'NONE', #29745, 19.99999999999998579 ) ;
#26139=EDGE_CURVE ( 'NONE', #31396, #5642, #12465, .T. ) ;
#26166=DIRECTION ( 'NONE',  ( 1.000000000000000000, -0.000000000000000000, -0.000000000000000000 ) ) ;
#26186=PLANE ( 'NONE',  #25233 ) ;
#26201=VECTOR ( 'NONE', #22563, 1000.000000000000000 ) ;
#26239=AXIS2_PLACEMENT_3D ( 'NONE', #30379, #5704, #16664 ) ;
#26251=CARTESIAN_POINT ( 'NONE',  ( 0.000000000000000000, 14.87816164169121080, -4.342730381189718436 ) ) ;
#26272=EDGE_CURVE ( 'NONE', #9129, #8057, #14451, .T. ) ;
#26281=CARTESIAN_POINT ( 'NONE',  ( 8.000000000000000000, 14.87816164169115218, 4.342730381189920941 ) ) ;
#26319=VECTOR ( 'NONE', #12092, 1000.000000000000000 ) ;
#26384=DIRECTION ( 'NONE',  ( -1.000000000000000000, 0.000000000000000000, 0.000000000000000000 ) ) ;
#26389=EDGE_CURVE ( 'NONE', #28254, #24948, #12238, .T. ) ;
#26393=DIRECTION ( 'NONE',  ( 0.000000000000000000, -0.6427876096865456912, 0.7660444431189726844 ) ) ;
#26394=CYLINDRICAL_SURFACE ( 'NONE', #32788, 7.199999999999993960 ) ;
#26399=ORIENTED_EDGE ( 'NONE', *, *, #2269, .T. ) ;
#26411=CARTESIAN_POINT ( 'NONE',  ( 8.000000000000000000, -15.46619997295641369, -1.007799283846847471 ) ) ;
#26421=EDGE_CURVE ( 'NONE', #7183, #20895, #25100, .T. ) ;
#26435=CARTESIAN_POINT ( 'NONE',  ( 8.000000000000000000, -5.482169781018935595, 16.00140663693123599 ) ) ;
#26475=CARTESIAN_POINT ( 'NONE',  ( 8.000000000000000000, -6.860320204751044315, -13.89802171851389900 ) ) ;
#26479=AXIS2_PLACEMENT_3D ( 'NONE', #754, #3303, #11920 ) ;
#26482=DIRECTION ( 'NONE',  ( 0.000000000000000000, 0.000000000000000000, 1.000000000000000000 ) ) ;
#26490=CARTESIAN_POINT ( 'NONE',  ( 8.000000000000000000, -14.87816164169118416, 4.342730381189816136 ) ) ;
#26491=CARTESIAN_POINT ( 'NONE',  ( 8.000000000000000000, 0.000000000000000000, 4.000000000000000000 ) ) ;
#26492=ORIENTED_EDGE ( 'NONE', *, *, #32076, .T. ) ;
#26498=CIRCLE ( 'NONE', #24201, 19.99999999999998579 ) ;
#26501=ADVANCED_FACE ( 'NONE', ( #29370 ), #4715, .T. ) ;
#26504=CARTESIAN_POINT ( 'NONE',  ( 0.000000000000000000, 0.3212489022567689423, -16.91141623315866482 ) ) ;
#26506=ORIENTED_EDGE ( 'NONE', *, *, #28893, .T. ) ;
#26542=ORIENTED_EDGE ( 'NONE', *, *, #7792, .T. ) ;
#26547=ORIENTED_EDGE ( 'NONE', *, *, #4066, .T. ) ;
#26579=CIRCLE ( 'NONE', #3014, 7.199999999999986855 ) ;
#26582=EDGE_LOOP ( 'NONE', ( #32085, #2196, #15528, #32109 ) ) ;
#26589=CARTESIAN_POINT ( 'NONE',  ( 0.000000000000000000, 0.000000000000000000, 0.000000000000000000 ) ) ;
#26599=AXIS2_PLACEMENT_3D ( 'NONE', #9938, #4379, #7235 ) ;
#26602=ORIENTED_EDGE ( 'NONE', *, *, #1583, .F. ) ;
#26609=DIRECTION ( 'NONE',  ( 0.000000000000000000, 0.000000000000000000, 1.000000000000000000 ) ) ;
#26625=VERTEX_POINT ( 'NONE', #26491 ) ;
#26626=ORIENTED_EDGE ( 'NONE', *, *, #24730, .T. ) ;
#26628=EDGE_CURVE ( 'NONE', #27701, #16891, #14618, .T. ) ;
#26633=EDGE_CURVE ( 'NONE', #20288, #13349, #31315, .T. ) ;
#26646=CARTESIAN_POINT ( 'NONE',  ( 8.000000000000000000, 10.62435788049461571, -13.16139124467909483 ) ) ;
#26659=ADVANCED_FACE ( 'NONE', ( #2543 ), #14201, .T. ) ;
#26663=DIRECTION ( 'NONE',  ( -1.000000000000000000, 0.000000000000000000, 0.000000000000000000 ) ) ;
#26725=VERTEX_POINT ( 'NONE', #35479 ) ;
#26731=AXIS2_PLACEMENT_3D ( 'NONE', #6949, #23151, #12539 ) ;
#26732=CIRCLE ( 'NONE', #23258, 7.200000000000000178 ) ;
#26737=DIRECTION ( 'NONE',  ( 0.000000000000000000, 0.000000000000000000, 1.000000000000000000 ) ) ;
#26749=DIRECTION ( 'NONE',  ( 1.000000000000000000, -0.000000000000000000, -0.000000000000000000 ) ) ;
#26759=CYLINDRICAL_SURFACE ( 'NONE', #29149, 15.49899999999998457 ) ;
#26760=VERTEX_POINT ( 'NONE', #9334 ) ;
#26761=ORIENTED_EDGE ( 'NONE', *, *, #9286, .T. ) ;
#26775=ORIENTED_EDGE ( 'NONE', *, *, #2696, .F. ) ;
#26791=CARTESIAN_POINT ( 'NONE',  ( 8.000000000000000000, -6.860320204751237938, 13.89802171851381551 ) ) ;
#26799=CARTESIAN_POINT ( 'NONE',  ( 4.000000000000000000, 19.60123832284017453, 3.973846525876501889 ) ) ;
#26800=ORIENTED_EDGE ( 'NONE', *, *, #20212, .T. ) ;
#26823=CARTESIAN_POINT ( 'NONE',  ( 8.000000000000000000, -16.59870953437682672, 3.253005020243791456 ) ) ;
#26841=CIRCLE ( 'NONE', #19902, 15.49899999999998279 ) ;
#26843=VERTEX_POINT ( 'NONE', #23369 ) ;
#26851=CARTESIAN_POINT ( 'NONE',  ( 0.000000000000000000, -8.605879768205133118, -12.89022243466717299 ) ) ;
#26852=ORIENTED_EDGE ( 'NONE', *, *, #9094, .F. ) ;
#26875=EDGE_CURVE ( 'NONE', #5458, #192, #11748, .T. ) ;
#26884=DIRECTION ( 'NONE',  ( 0.000000000000000000, 0.000000000000000000, 1.000000000000000000 ) ) ;
#26893=VECTOR ( 'NONE', #30342, 1000.000000000000000 ) ;
#26915=AXIS2_PLACEMENT_3D ( 'NONE', #31631, #6966, #31811 ) ;
#26919=DIRECTION ( 'NONE',  ( 1.000000000000000000, -0.000000000000000000, 0.000000000000000000 ) ) ;
#26938=DIRECTION ( 'NONE',  ( -1.000000000000000000, 0.000000000000000000, 0.000000000000000000 ) ) ;
#26940=DIRECTION ( 'NONE',  ( 0.000000000000000000, -0.6427876096865456912, 0.7660444431189726844 ) ) ;
#26948=DIRECTION ( 'NONE',  ( 0.000000000000000000, 0.000000000000000000, 1.000000000000000000 ) ) ;
#26953=VERTEX_POINT ( 'NONE', #15779 ) ;
#26956=ORIENTED_EDGE ( 'NONE', *, *, #878, .F. ) ;
#26963=VERTEX_POINT ( 'NONE', #7687 ) ;
#26998=VERTEX_POINT ( 'NONE', #4305 ) ;
#27007=AXIS2_PLACEMENT_3D ( 'NONE', #17937, #28937, #1391 ) ;
#27014=ORIENTED_EDGE ( 'NONE', *, *, #13687, .F. ) ;
#27027=ORIENTED_EDGE ( 'NONE', *, *, #10653, .T. ) ;
#27041=ORIENTED_EDGE ( 'NONE', *, *, #29961, .T. ) ;
#27046=DIRECTION ( 'NONE',  ( 0.000000000000000000, 0.000000000000000000, 1.000000000000000000 ) ) ;
#27053=DIRECTION ( 'NONE',  ( -1.000000000000000000, 0.000000000000000000, 0.000000000000000000 ) ) ;
#27063=EDGE_LOOP ( 'NONE', ( #5889, #13949, #30912, #26506 ) ) ;
#27068=CIRCLE ( 'NONE', #17840, 7.199999999999993072 ) ;
#27077=EDGE_CURVE ( 'NONE', #656, #21748, #20388, .T. ) ;
#27111=AXIS2_PLACEMENT_3D ( 'NONE', #29126, #31466, #32176 ) ;
#27123=ADVANCED_FACE ( 'NONE', ( #10761 ), #13464, .T. ) ;
#27124=EDGE_LOOP ( 'NONE', ( #30952, #27207, #30520, #26852 ) ) ;
#27131=DIRECTION ( 'NONE',  ( -1.000000000000000000, 0.000000000000000000, 0.000000000000000000 ) ) ;
#27147=DIRECTION ( 'NONE',  ( 0.000000000000000000, -0.3420201433256564449, -0.9396926207859127578 ) ) ;
#27192=FACE_OUTER_BOUND ( 'NONE', #30288, .T. ) ;
#27195=CARTESIAN_POINT ( 'NONE',  ( 8.000000000000000000, 6.860320204751148232, 13.89802171851385459 ) ) ;
#27202=DIRECTION ( 'NONE',  ( -1.000000000000000000, 0.000000000000000000, 0.000000000000000000 ) ) ;
#27207=ORIENTED_EDGE ( 'NONE', *, *, #32220, .T. ) ;
#27211=LINE ( 'NONE', #21251, #21105 ) ;
#27221=VECTOR ( 'NONE', #15335, 1000.000000000000000 ) ;
#27231=CYLINDRICAL_SURFACE ( 'NONE', #10137, 7.199999999999994849 ) ;
#27235=ORIENTED_EDGE ( 'NONE', *, *, #19805, .T. ) ;
#27238=CARTESIAN_POINT ( 'NONE',  ( 0.000000000000000000, -13.24207120356975587, 14.98824707027438485 ) ) ;
#27245=DIRECTION ( 'NONE',  ( -1.000000000000000000, 0.000000000000000000, 0.000000000000000000 ) ) ;
#27300=FACE_OUTER_BOUND ( 'NONE', #3825, .T. ) ;
#27309=FACE_OUTER_BOUND ( 'NONE', #25843, .T. ) ;
#27318=AXIS2_PLACEMENT_3D ( 'NONE', #8049, #30385, #24802 ) ;
#27336=ORIENTED_EDGE ( 'NONE', *, *, #15343, .T. ) ;
#27364=CARTESIAN_POINT ( 'NONE',  ( 8.000000000000000000, 0.000000000000000000, 0.000000000000000000 ) ) ;
#27368=ORIENTED_EDGE ( 'NONE', *, *, #13134, .T. ) ;
#27370=VERTEX_POINT ( 'NONE', #3381 ) ;
#27381=ORIENTED_EDGE ( 'NONE', *, *, #16571, .F. ) ;
#27384=DIRECTION ( 'NONE',  ( -1.000000000000000000, 0.000000000000000000, 0.000000000000000000 ) ) ;
#27392=ORIENTED_EDGE ( 'NONE', *, *, #6242, .F. ) ;
#27429=ORIENTED_EDGE ( 'NONE', *, *, #20539, .F. ) ;
#27455=AXIS2_PLACEMENT_3D ( 'NONE', #19812, #20347, #17481 ) ;
#27459=MECHANICAL_DESIGN_GEOMETRIC_PRESENTATION_REPRESENTATION('',(#30331),#10207);
#27474=DIRECTION ( 'NONE',  ( 0.000000000000000000, 0.000000000000000000, 1.000000000000000000 ) ) ;
#27492=ORIENTED_EDGE ( 'NONE', *, *, #3623, .T. ) ;
#27498=CARTESIAN_POINT ( 'NONE',  ( 0.000000000000000000, -19.60123832284014611, -3.973846525876633340 ) ) ;
#27504=DIRECTION ( 'NONE',  ( 0.000000000000000000, 0.3420201433256695456, -0.9396926207859079838 ) ) ;
#27526=DIRECTION ( 'NONE',  ( 0.000000000000000000, 0.000000000000000000, -1.000000000000000000 ) ) ;
#27530=DIRECTION ( 'NONE',  ( -1.000000000000000000, 0.000000000000000000, 0.000000000000000000 ) ) ;
#27555=DIRECTION ( 'NONE',  ( -1.000000000000000000, 0.000000000000000000, 0.000000000000000000 ) ) ;
#27557=VERTEX_POINT ( 'NONE', #10369 ) ;
#27562=CARTESIAN_POINT ( 'NONE',  ( 8.000000000000000000, 17.56975900509174693, 9.555290079479316745 ) ) ;
#27566=DIRECTION ( 'NONE',  ( 0.000000000000000000, 0.6427876096865403621, -0.7660444431189771253 ) ) ;
#27587=AXIS2_PLACEMENT_3D ( 'NONE', #8490, #25594, #207 ) ;
#27618=EDGE_CURVE ( 'NONE', #28712, #21743, #29817, .T. ) ;
#27635=LINE ( 'NONE', #5314, #28434 ) ;
#27653=CARTESIAN_POINT ( 'NONE',  ( 8.000000000000000000, 14.80634052301623171, 8.177498406287277533 ) ) ;
#27661=VERTEX_POINT ( 'NONE', #18992 ) ;
#27670=DIRECTION ( 'NONE',  ( -1.000000000000000000, 0.000000000000000000, 0.000000000000000000 ) ) ;
#27673=LINE ( 'NONE', #19023, #28023 ) ;
#27680=ORIENTED_EDGE ( 'NONE', *, *, #274, .T. ) ;
#27692=CYLINDRICAL_SURFACE ( 'NONE', #14053, 15.49899999999998457 ) ;
#27693=VERTEX_POINT ( 'NONE', #21686 ) ;
#27700=CYLINDRICAL_SURFACE ( 'NONE', #30573, 15.49899999999998457 ) ;
#27701=VERTEX_POINT ( 'NONE', #24764 ) ;
#27716=CARTESIAN_POINT ( 'NONE',  ( 8.000000000000000000, 15.46619997295642079, 1.007799283846740002 ) ) ;
#27730=DIRECTION ( 'NONE',  ( -1.000000000000000000, 0.000000000000000000, 0.000000000000000000 ) ) ;
#27735=EDGE_CURVE ( 'NONE', #21409, #31574, #9071, .T. ) ;
#27738=ORIENTED_EDGE ( 'NONE', *, *, #2245, .T. ) ;
#27746=CARTESIAN_POINT ( 'NONE',  ( 8.000000000000000000, -8.605879768205326741, 12.89022243466705930 ) ) ;
#27777=CARTESIAN_POINT ( 'NONE',  ( 8.000000000000000000, -14.87816164169111310, -4.342730381190021305 ) ) ;
#27792=CYLINDRICAL_SURFACE ( 'NONE', #32691, 7.199999999999993960 ) ;
#27794=EDGE_CURVE ( 'NONE', #11433, #15563, #7817, .T. ) ;
#27816=FACE_OUTER_BOUND ( 'NONE', #10541, .T. ) ;
#27861=DIRECTION ( 'NONE',  ( 0.000000000000000000, 0.000000000000000000, 1.000000000000000000 ) ) ;
#27866=ORIENTED_EDGE ( 'NONE', *, *, #28201, .T. ) ;
#27905=ORIENTED_EDGE ( 'NONE', *, *, #15901, .T. ) ;
#27908=CIRCLE ( 'NONE', #28500, 7.199999999999998401 ) ;
#27931=DIRECTION ( 'NONE',  ( -1.000000000000000000, 0.000000000000000000, 0.000000000000000000 ) ) ;
#27943=DIRECTION ( 'NONE',  ( -1.000000000000000000, 0.000000000000000000, 0.000000000000000000 ) ) ;
#27958=EDGE_CURVE ( 'NONE', #1241, #13855, #10709, .T. ) ;
#27971=DIRECTION ( 'NONE',  ( 0.000000000000000000, 0.000000000000000000, -1.000000000000000000 ) ) ;
#28008=DIRECTION ( 'NONE',  ( -1.000000000000000000, 0.000000000000000000, 0.000000000000000000 ) ) ;
#28012=VECTOR ( 'NONE', #10531, 1000.000000000000000 ) ;
#28023=VECTOR ( 'NONE', #5357, 1000.000000000000000 ) ;
#28047=DIRECTION ( 'NONE',  ( 0.000000000000000000, -0.3420201433256564449, -0.9396926207859127578 ) ) ;
#28064=DIRECTION ( 'NONE',  ( -1.000000000000000000, 0.000000000000000000, 0.000000000000000000 ) ) ;
#28065=DIRECTION ( 'NONE',  ( -1.000000000000000000, 0.000000000000000000, 0.000000000000000000 ) ) ;
#28071=VECTOR ( 'NONE', #20297, 1000.000000000000000 ) ;
#28086=VERTEX_POINT ( 'NONE', #11153 ) ;
#28095=ORIENTED_EDGE ( 'NONE', *, *, #6406, .F. ) ;
#28115=CARTESIAN_POINT ( 'NONE',  ( 0.000000000000000000, 7.317194182740413666, -18.61340026142641690 ) ) ;
#28116=ORIENTED_EDGE ( 'NONE', *, *, #7540, .T. ) ;
#28119=ADVANCED_FACE ( 'NONE', ( #16712 ), #11500, .T. ) ;
#28199=FACE_OUTER_BOUND ( 'NONE', #10260, .T. ) ;
#28201=EDGE_CURVE ( 'NONE', #22597, #17024, #23928, .T. ) ;
#28204=ORIENTED_EDGE ( 'NONE', *, *, #6011, .F. ) ;
#28209=DIRECTION ( 'NONE',  ( 0.000000000000000000, -0.8660254037844433705, 0.4999999999999918954 ) ) ;
#28210=ORIENTED_EDGE ( 'NONE', *, *, #26633, .T. ) ;
#28223=CARTESIAN_POINT ( 'NONE',  ( 8.000000000000000000, 0.000000000000000000, 0.000000000000000000 ) ) ;
#28237=DIRECTION ( 'NONE',  ( -1.000000000000000000, 0.000000000000000000, 0.000000000000000000 ) ) ;
#28254=VERTEX_POINT ( 'NONE', #4301 ) ;
#28283=ORIENTED_EDGE ( 'NONE', *, *, #13714, .F. ) ;
#28288=VERTEX_POINT ( 'NONE', #3586 ) ;
#28299=ADVANCED_FACE ( 'NONE', ( #25549 ), #11846, .T. ) ;
#28302=CARTESIAN_POINT ( 'NONE',  ( -10.00000000000000000, 0.000000000000000000, 0.000000000000000000 ) ) ;
#28311=CARTESIAN_POINT ( 'NONE',  ( 0.000000000000000000, 6.071532165918824830E-15, 1.000000000000000000 ) ) ;
#28312=CIRCLE ( 'NONE', #25443, 15.49899999999998634 ) ;
#28315=ORIENTED_EDGE ( 'NONE', *, *, #3980, .F. ) ;
#28332=LINE ( 'NONE', #6895, #6631 ) ;
#28342=ORIENTED_EDGE ( 'NONE', *, *, #714, .T. ) ;
#28345=VERTEX_POINT ( 'NONE', #10040 ) ;
#28353=DIRECTION ( 'NONE',  ( -1.000000000000000000, 0.000000000000000000, 0.000000000000000000 ) ) ;
#28358=EDGE_CURVE ( 'NONE', #29334, #5158, #7514, .T. ) ;
#28393=DIRECTION ( 'NONE',  ( 0.000000000000000000, -0.9848077530122097967, 0.1736481776669208388 ) ) ;
#28394=ORIENTED_EDGE ( 'NONE', *, *, #16264, .T. ) ;
#28398=DIRECTION ( 'NONE',  ( -1.000000000000000000, 0.000000000000000000, 0.000000000000000000 ) ) ;
#28406=CARTESIAN_POINT ( 'NONE',  ( 0.000000000000000000, 0.000000000000000000, 0.000000000000000000 ) ) ;
#28418=CARTESIAN_POINT ( 'NONE',  ( 8.000000000000000000, 11.11653975335807587, -12.74840161668719851 ) ) ;
#28420=DIRECTION ( 'NONE',  ( 0.000000000000000000, -0.3420201433256756518, 0.9396926207859058744 ) ) ;
#28421=ORIENTED_EDGE ( 'NONE', *, *, #26127, .F. ) ;
#28434=VECTOR ( 'NONE', #6312, 1000.000000000000000 ) ;
#28443=VERTEX_POINT ( 'NONE', #9858 ) ;
#28448=ADVANCED_FACE ( 'NONE', ( #21196 ), #13121, .T. ) ;
#28489=ADVANCED_FACE ( 'NONE', ( #10936 ), #30026, .T. ) ;
#28497=CARTESIAN_POINT ( 'NONE',  ( 0.000000000000000000, -10.62435788049434038, -13.16139124467930444 ) ) ;
#28500=AXIS2_PLACEMENT_3D ( 'NONE', #21761, #11150, #24835 ) ;
#28505=ORIENTED_EDGE ( 'NONE', *, *, #26272, .T. ) ;
#28508=CIRCLE ( 'NONE', #12997, 7.199999999999992184 ) ;
#28523=ORIENTED_EDGE ( 'NONE', *, *, #33440, .T. ) ;
#28537=CARTESIAN_POINT ( 'NONE',  ( 8.000000000000000000, -13.24207120356955159, -14.98824707027454828 ) ) ;
#28544=CIRCLE ( 'NONE', #18208, 7.200000000000000178 ) ;
#28555=CYLINDRICAL_SURFACE ( 'NONE', #20985, 15.49899999999998457 ) ;
#28583=FACE_OUTER_BOUND ( 'NONE', #20894, .T. ) ;
#28596=EDGE_CURVE ( 'NONE', #6533, #12194, #2668, .T. ) ;
#28602=CIRCLE ( 'NONE', #10773, 19.99999999999998579 ) ;
#28606=CIRCLE ( 'NONE', #9063, 7.199999999999998401 ) ;
#28607=DIRECTION ( 'NONE',  ( 0.000000000000000000, 0.8660254037844364872, 0.5000000000000036637 ) ) ;
#28626=DIRECTION ( 'NONE',  ( 0.000000000000000000, 0.000000000000000000, 1.000000000000000000 ) ) ;
#28637=CARTESIAN_POINT ( 'NONE',  ( 8.000000000000000000, 0.000000000000000000, 0.000000000000000000 ) ) ;
#28652=ORIENTED_EDGE ( 'NONE', *, *, #10109, .T. ) ;
#28663=AXIS2_PLACEMENT_3D ( 'NONE', #3029, #5717, #19388 ) ;
#28665=DIRECTION ( 'NONE',  ( -1.000000000000000000, 0.000000000000000000, 0.000000000000000000 ) ) ;
#28693=FACE_OUTER_BOUND ( 'NONE', #26582, .T. ) ;
#28697=CARTESIAN_POINT ( 'NONE',  ( 8.000000000000000000, -15.46619997295641369, -1.007799283846847471 ) ) ;
#28712=VERTEX_POINT ( 'NONE', #9287 ) ;
#28733=CYLINDRICAL_SURFACE ( 'NONE', #16949, 7.199999999999994849 ) ;
#28734=CARTESIAN_POINT ( 'NONE',  ( 0.000000000000000000, -6.085920226790910270, -15.78165944574524637 ) ) ;
#28736=CARTESIAN_POINT ( 'NONE',  ( 8.000000000000000000, 0.000000000000000000, 0.000000000000000000 ) ) ;
#28756=DIRECTION ( 'NONE',  ( -1.000000000000000000, 0.000000000000000000, 0.000000000000000000 ) ) ;
#28779=AXIS2_PLACEMENT_3D ( 'NONE', #13777, #5496, #8179 ) ;
#28780=CIRCLE ( 'NONE', #17841, 7.199999999999993960 ) ;
#28836=VERTEX_POINT ( 'NONE', #7115 ) ;
#28839=EDGE_CURVE ( 'NONE', #8462, #10099, #20960, .T. ) ;
#28849=EDGE_CURVE ( 'NONE', #8462, #32097, #33757, .T. ) ;
#28853=EDGE_CURVE ( 'NONE', #19590, #1645, #21494, .T. ) ;
#28858=CARTESIAN_POINT ( 'NONE',  ( 8.000000000000000000, -16.71027810728550733, -2.620268201066114688 ) ) ;
#28859=ORIENTED_EDGE ( 'NONE', *, *, #30365, .F. ) ;
#28865=EDGE_LOOP ( 'NONE', ( #1478, #32875, #19662, #31612 ) ) ;
#28871=DIRECTION ( 'NONE',  ( -1.000000000000000000, 0.000000000000000000, 0.000000000000000000 ) ) ;
#28889=FACE_OUTER_BOUND ( 'NONE', #12259, .T. ) ;
#28890=DIRECTION ( 'NONE',  ( 0.000000000000000000, 0.000000000000000000, 1.000000000000000000 ) ) ;
#28893=EDGE_CURVE ( 'NONE', #32097, #14060, #34911, .T. ) ;
#28902=AXIS2_PLACEMENT_3D ( 'NONE', #13571, #32835, #2794 ) ;
#28910=DIRECTION ( 'NONE',  ( -1.000000000000000000, 0.000000000000000000, 0.000000000000000000 ) ) ;
#28918=ORIENTED_EDGE ( 'NONE', *, *, #14550, .T. ) ;
#28933=CARTESIAN_POINT ( 'NONE',  ( -10.00000000000000000, 0.000000000000000000, 19.99999999999998579 ) ) ;
#28937=DIRECTION ( 'NONE',  ( -1.000000000000000000, 0.000000000000000000, 0.000000000000000000 ) ) ;
#28940=VECTOR ( 'NONE', #4518, 1000.000000000000000 ) ;
#28950=CARTESIAN_POINT ( 'NONE',  ( 0.000000000000000000, 11.11653975335790179, 12.74840161668735661 ) ) ;
#28955=DIRECTION ( 'NONE',  ( 0.000000000000000000, 0.3420201433256695456, -0.9396926207859079838 ) ) ;
#28956=ORIENTED_EDGE ( 'NONE', *, *, #12062, .F. ) ;
#28961=ORIENTED_EDGE ( 'NONE', *, *, #12303, .T. ) ;
#28966=ORIENTED_EDGE ( 'NONE', *, *, #27735, .T. ) ;
#28979=DIRECTION ( 'NONE',  ( 0.000000000000000000, 0.000000000000000000, 1.000000000000000000 ) ) ;
#28997=DIRECTION ( 'NONE',  ( -1.000000000000000000, 0.000000000000000000, 0.000000000000000000 ) ) ;
#29035=DIRECTION ( 'NONE',  ( -1.000000000000000000, 0.000000000000000000, 0.000000000000000000 ) ) ;
#29045=CARTESIAN_POINT ( 'NONE',  ( 0.000000000000000000, -6.085920226791118992, 15.78165944574518775 ) ) ;
#29048=CARTESIAN_POINT ( 'NONE',  ( 8.000000000000000000, 5.482169781018835231, 16.00140663693125376 ) ) ;
#29065=AXIS2_PLACEMENT_3D ( 'NONE', #10688, #5123, #2254 ) ;
#29084=EDGE_CURVE ( 'NONE', #34283, #13349, #19332, .T. ) ;
#29088=CARTESIAN_POINT ( 'NONE',  ( 8.000000000000000000, -12.46108038583322930, 15.64357617738992801 ) ) ;
#29089=DIRECTION ( 'NONE',  ( 0.000000000000000000, -8.881784197001252323E-16, 1.000000000000000000 ) ) ;
#29090=ADVANCED_FACE ( 'NONE', ( #11241 ), #5153, .T. ) ;
#29091=DIRECTION ( 'NONE',  ( -1.000000000000000000, 0.000000000000000000, 0.000000000000000000 ) ) ;
#29101=SURFACE_SIDE_STYLE ('',( #7306 ) ) ;
#29126=CARTESIAN_POINT ( 'NONE',  ( 8.000000000000000000, 10.62435788049461571, -13.16139124467909483 ) ) ;
#29149=AXIS2_PLACEMENT_3D ( 'NONE', #10371, #13595, #13255 ) ;
#29154=ORIENTED_EDGE ( 'NONE', *, *, #26628, .T. ) ;
#29165=EDGE_LOOP ( 'NONE', ( #3762, #27381, #11256, #20870 ) ) ;
#29174=CARTESIAN_POINT ( 'NONE',  ( 0.000000000000000000, -17.56975900509168298, -9.555290079479433984 ) ) ;
#29187=CARTESIAN_POINT ( 'NONE',  ( 0.000000000000000000, -6.860320204751044315, -13.89802171851389900 ) ) ;
#29207=LINE ( 'NONE', #18377, #24578 ) ;
#29209=ORIENTED_EDGE ( 'NONE', *, *, #33586, .F. ) ;
#29232=LINE ( 'NONE', #31564, #17352 ) ;
#29261=DIRECTION ( 'NONE',  ( -1.000000000000000000, 0.000000000000000000, 0.000000000000000000 ) ) ;
#29299=CYLINDRICAL_SURFACE ( 'NONE', #27007, 15.49899999999998457 ) ;
#29300=CIRCLE ( 'NONE', #4022, 7.199999999999993960 ) ;
#29314=DIRECTION ( 'NONE',  ( -1.000000000000000000, 0.000000000000000000, 0.000000000000000000 ) ) ;
#29325=ORIENTED_EDGE ( 'NONE', *, *, #13057, .F. ) ;
#29333=AXIS2_PLACEMENT_3D ( 'NONE', #35456, #35285, #29691 ) ;
#29334=VERTEX_POINT ( 'NONE', #35143 ) ;
#29348=CARTESIAN_POINT ( 'NONE',  ( 4.000000000000000000, -17.56975900509168298, -9.555290079479433984 ) ) ;
#29350=CARTESIAN_POINT ( 'NONE',  ( 8.000000000000000000, 10.62435788049443808, 13.16139124467922272 ) ) ;
#29370=FACE_OUTER_BOUND ( 'NONE', #31403, .T. ) ;
#29399=DIRECTION ( 'NONE',  ( 0.000000000000000000, 0.000000000000000000, 1.000000000000000000 ) ) ;
#29423=ORIENTED_EDGE ( 'NONE', *, *, #35444, .F. ) ;
#29437=CARTESIAN_POINT ( 'NONE',  ( 0.000000000000000000, 12.46108038583334299, -15.64357617738982142 ) ) ;
#29444=CARTESIAN_POINT ( 'NONE',  ( 4.000000000000000000, 12.46108038583314936, 15.64357617739001860 ) ) ;
#29450=CARTESIAN_POINT ( 'NONE',  ( 8.000000000000000000, 14.87816164169115218, 4.342730381189920941 ) ) ;
#29457=ORIENTED_EDGE ( 'NONE', *, *, #3046, .T. ) ;
#29479=DIRECTION ( 'NONE',  ( -1.000000000000000000, 0.000000000000000000, 0.000000000000000000 ) ) ;
#29493=CARTESIAN_POINT ( 'NONE',  ( 0.000000000000000000, 7.317194182740155206, 18.61340026142654125 ) ) ;
#29522=CIRCLE ( 'NONE', #3074, 7.199999999999993072 ) ;
#29551=EDGE_LOOP ( 'NONE', ( #6735, #32431, #14382, #10759 ) ) ;
#29564=EDGE_CURVE ( 'NONE', #21331, #31396, #8493, .T. ) ;
#29567=EDGE_LOOP ( 'NONE', ( #23142, #18146, #18960, #20423 ) ) ;
#29586=DIRECTION ( 'NONE',  ( -1.000000000000000000, 0.000000000000000000, 0.000000000000000000 ) ) ;
#29613=DIRECTION ( 'NONE',  ( -1.000000000000000000, 0.000000000000000000, 0.000000000000000000 ) ) ;
#29617=CARTESIAN_POINT ( 'NONE',  ( -10.00000000000000000, 0.000000000000000000, 0.000000000000000000 ) ) ;
#29640=DIRECTION ( 'NONE',  ( -1.000000000000000000, 0.000000000000000000, 0.000000000000000000 ) ) ;
#29641=ORIENTED_EDGE ( 'NONE', *, *, #35455, .T. ) ;
#29647=CARTESIAN_POINT ( 'NONE',  ( 8.000000000000000000, -11.11653975335780942, -12.74840161668743299 ) ) ;
#29665=DIRECTION ( 'NONE',  ( -1.000000000000000000, 0.000000000000000000, 0.000000000000000000 ) ) ;
#29676=ORIENTED_EDGE ( 'NONE', *, *, #2985, .T. ) ;
#29683=CARTESIAN_POINT ( 'NONE',  ( 8.000000000000000000, 16.59870953437685515, -3.253005020243678214 ) ) ;
#29691=DIRECTION ( 'NONE',  ( 0.000000000000000000, 0.000000000000000000, 1.000000000000000000 ) ) ;
#29698=VECTOR ( 'NONE', #20525, 1000.000000000000000 ) ;
#29707=DIRECTION ( 'NONE',  ( 0.000000000000000000, 0.000000000000000000, 1.000000000000000000 ) ) ;
#29714=ADVANCED_FACE ( 'NONE', ( #1247 ), #25563, .T. ) ;
#29745=AXIS2_PLACEMENT_3D ( 'NONE', #28302, #28665, #9030 ) ;
#29754=DIRECTION ( 'NONE',  ( -1.000000000000000000, 0.000000000000000000, 0.000000000000000000 ) ) ;
#29761=DIRECTION ( 'NONE',  ( 0.000000000000000000, 0.000000000000000000, 1.000000000000000000 ) ) ;
#29770=CIRCLE ( 'NONE', #6745, 7.199999999999993072 ) ;
#29778=ORIENTED_EDGE ( 'NONE', *, *, #12817, .T. ) ;
#29781=( LENGTH_UNIT ( ) NAMED_UNIT ( * ) SI_UNIT ( .MILLI., .METRE. ) );
#29794=CIRCLE ( 'NONE', #15391, 19.99999999999998579 ) ;
#29798=CARTESIAN_POINT ( 'NONE',  ( 8.000000000000000000, 11.19999565274250308, 10.71350075272077973 ) ) ;
#29803=ORIENTED_EDGE ( 'NONE', *, *, #34012, .F. ) ;
#29809=LINE ( 'NONE', #13586, #28012 ) ;
#29817=LINE ( 'NONE', #5155, #6073 ) ;
#29847=DIRECTION ( 'NONE',  ( -1.000000000000000000, 0.000000000000000000, 0.000000000000000000 ) ) ;
#29880=DIRECTION ( 'NONE',  ( 0.000000000000000000, 0.000000000000000000, 1.000000000000000000 ) ) ;
#29883=EDGE_CURVE ( 'NONE', #22477, #33707, #25780, .T. ) ;
#29906=LINE ( 'NONE', #5074, #18234 ) ;
#29917=EDGE_CURVE ( 'NONE', #11373, #21654, #10251, .T. ) ;
#29921=PRODUCT_DEFINITION_FORMATION_WITH_SPECIFIED_SOURCE ( 'ANY', '', #7526, .NOT_KNOWN. ) ;
#29931=LINE ( 'NONE', #15329, #4901 ) ;
#29936=CARTESIAN_POINT ( 'NONE',  ( 8.000000000000000000, 16.71027810728549667, 2.620268201066223934 ) ) ;
#29938=AXIS2_PLACEMENT_3D ( 'NONE', #26435, #10405, #15593 ) ;
#29954=( NAMED_UNIT ( * ) SI_UNIT ( $, .STERADIAN. ) SOLID_ANGLE_UNIT ( ) );
#29955=CARTESIAN_POINT ( 'NONE',  ( 8.000000000000000000, -6.085920226790910270, -15.78165944574524637 ) ) ;
#29956=ORIENTED_EDGE ( 'NONE', *, *, #30477, .T. ) ;
#29961=EDGE_CURVE ( 'NONE', #15563, #33313, #31831, .T. ) ;
#29975=DIRECTION ( 'NONE',  ( -1.000000000000000000, 0.000000000000000000, 0.000000000000000000 ) ) ;
#29985=DIRECTION ( 'NONE',  ( 0.000000000000000000, -0.6427876096865295930, -0.7660444431189862291 ) ) ;
#30011=ORIENTED_EDGE ( 'NONE', *, *, #33674, .F. ) ;
#30022=CARTESIAN_POINT ( 'NONE',  ( 8.000000000000000000, -19.60123832284014966, -3.973846525876632008 ) ) ;
#30024=DIRECTION ( 'NONE',  ( 0.000000000000000000, -0.9848077530122096857, 0.1736481776669208388 ) ) ;
#30026=CYLINDRICAL_SURFACE ( 'NONE', #30272, 7.199999999999994849 ) ;
#30042=FACE_OUTER_BOUND ( 'NONE', #19607, .T. ) ;
#30045=ADVANCED_FACE ( 'NONE', ( #30042 ), #16859, .T. ) ;
#30049=ORIENTED_EDGE ( 'NONE', *, *, #21370, .T. ) ;
#30050=CARTESIAN_POINT ( 'NONE',  ( 8.000000000000000000, 0.000000000000000000, 0.000000000000000000 ) ) ;
#30061=CARTESIAN_POINT ( 'NONE',  ( 4.000000000000000000, -12.46108038583323285, 15.64357617738992801 ) ) ;
#30067=ORIENTED_EDGE ( 'NONE', *, *, #14799, .F. ) ;
#30073=ORIENTED_EDGE ( 'NONE', *, *, #35286, .T. ) ;
#30085=VECTOR ( 'NONE', #112, 1000.000000000000000 ) ;
#30086=DIRECTION ( 'NONE',  ( -0.000000000000000000, 1.000000000000000000, 0.000000000000000000 ) ) ;
#30091=AXIS2_PLACEMENT_3D ( 'NONE', #14583, #27931, #30985 ) ;
#30102=DIRECTION ( 'NONE',  ( 0.000000000000000000, 0.000000000000000000, 1.000000000000000000 ) ) ;
#30110=CARTESIAN_POINT ( 'NONE',  ( 8.000000000000000000, 5.400000000000000355, 0.000000000000000000 ) ) ;
#30129=VERTEX_POINT ( 'NONE', #31930 ) ;
#30133=CARTESIAN_POINT ( 'NONE',  ( 50.00005079999999680, 5.400000000000000355, -0.9999999999999985567 ) ) ;
#30150=CARTESIAN_POINT ( 'NONE',  ( 8.000000000000000000, 17.56975900509189970, -9.555290079479078713 ) ) ;
#30176=EDGE_LOOP ( 'NONE', ( #22849, #13128, #13224, #27336 ) ) ;
#30179=EDGE_LOOP ( 'NONE', ( #22932, #1109, #5238, #6152 ) ) ;
#30186=VECTOR ( 'NONE', #7653, 1000.000000000000000 ) ;
#30205=ORIENTED_EDGE ( 'NONE', *, *, #19670, .F. ) ;
#30216=DIRECTION ( 'NONE',  ( 1.000000000000000000, -0.000000000000000000, 0.000000000000000000 ) ) ;
#30221=CIRCLE ( 'NONE', #23316, 7.199999999999992184 ) ;
#30229=EDGE_CURVE ( 'NONE', #28288, #19816, #10150, .T. ) ;
#30246=EDGE_CURVE ( 'NONE', #20111, #8462, #20393, .T. ) ;
#30261=CARTESIAN_POINT ( 'NONE',  ( 8.000000000000000000, 19.60123832284022782, -3.973846525876241653 ) ) ;
#30272=AXIS2_PLACEMENT_3D ( 'NONE', #121, #22422, #21902 ) ;
#30281=AXIS2_PLACEMENT_3D ( 'NONE', #22350, #27943, #6502 ) ;
#30288=EDGE_LOOP ( 'NONE', ( #3161, #32155, #17674, #18902 ) ) ;
#30315=DIRECTION ( 'NONE',  ( 0.000000000000000000, 0.000000000000000000, 1.000000000000000000 ) ) ;
#30329=VECTOR ( 'NONE', #16447, 1000.000000000000000 ) ;
#30331=STYLED_ITEM ( 'NONE', ( #10007 ), #34287 ) ;
#30341=DIRECTION ( 'NONE',  ( -1.000000000000000000, 0.000000000000000000, 0.000000000000000000 ) ) ;
#30342=DIRECTION ( 'NONE',  ( -1.000000000000000000, 0.000000000000000000, 0.000000000000000000 ) ) ;
#30365=EDGE_CURVE ( 'NONE', #20288, #21409, #24464, .T. ) ;
#30369=CARTESIAN_POINT ( 'NONE',  ( 8.000000000000000000, -11.19999565274257414, 10.71350075272070512 ) ) ;
#30375=AXIS2_PLACEMENT_3D ( 'NONE', #2508, #16149, #24285 ) ;
#30379=CARTESIAN_POINT ( 'NONE',  ( -10.00000000000000000, 0.000000000000000000, 0.000000000000000000 ) ) ;
#30385=DIRECTION ( 'NONE',  ( -1.000000000000000000, 0.000000000000000000, 0.000000000000000000 ) ) ;
#30397=AXIS2_PLACEMENT_3D ( 'NONE', #29647, #27131, #21883 ) ;
#30420=LINE ( 'NONE', #27716, #12086 ) ;
#30434=CARTESIAN_POINT ( 'NONE',  ( 8.000000000000000000, -6.085920226791118992, 15.78165944574518775 ) ) ;
#30459=CIRCLE ( 'NONE', #7446, 7.199999999999993072 ) ;
#30468=DIRECTION ( 'NONE',  ( 0.000000000000000000, -0.6427876096865294819, -0.7660444431189861181 ) ) ;
#30477=EDGE_CURVE ( 'NONE', #22707, #211, #12981, .T. ) ;
#30479=AXIS2_PLACEMENT_3D ( 'NONE', #17048, #6260, #16527 ) ;
#30505=CIRCLE ( 'NONE', #14959, 15.49899999999998279 ) ;
#30512=CARTESIAN_POINT ( 'NONE',  ( 8.000000000000000000, 6.860320204751340079, -13.89802171851375689 ) ) ;
#30520=ORIENTED_EDGE ( 'NONE', *, *, #32571, .F. ) ;
#30521=AXIS2_PLACEMENT_3D ( 'NONE', #29350, #21034, #7546 ) ;
#30528=CIRCLE ( 'NONE', #1205, 7.199999999999995737 ) ;
#30532=CARTESIAN_POINT ( 'NONE',  ( 0.000000000000000000, 5.482169781019050170, -16.00140663693117560 ) ) ;
#30545=CARTESIAN_POINT ( 'NONE',  ( 50.00005079999999680, 5.400000000000000355, 0.9999999999999985567 ) ) ;
#30556=EDGE_CURVE ( 'NONE', #21743, #7443, #30221, .T. ) ;
#30573=AXIS2_PLACEMENT_3D ( 'NONE', #13658, #3036, #22275 ) ;
#30575=CYLINDRICAL_SURFACE ( 'NONE', #10399, 7.199999999999994849 ) ;
#30584=CIRCLE ( 'NONE', #683, 7.199999999999998401 ) ;
#30599=EDGE_CURVE ( 'NONE', #8057, #6961, #3476, .T. ) ;
#30638=AXIS2_PLACEMENT_3D ( 'NONE', #25138, #465, #8728 ) ;
#30769=ORIENTED_EDGE ( 'NONE', *, *, #20217, .T. ) ;
#30772=DIRECTION ( 'NONE',  ( 0.000000000000000000, -6.987080667128811173E-15, 1.000000000000000000 ) ) ;
#30775=CYLINDRICAL_SURFACE ( 'NONE', #19010, 7.199999999999994849 ) ;
#30812=CARTESIAN_POINT ( 'NONE',  ( 8.000000000000000000, 14.80634052301623171, -8.177498406287266874 ) ) ;
#30824=EDGE_CURVE ( 'NONE', #34828, #34524, #1206, .T. ) ;
#30826=DIRECTION ( 'NONE',  ( 0.000000000000000000, 0.6427876096865403621, -0.7660444431189772363 ) ) ;
#30838=DIRECTION ( 'NONE',  ( 0.000000000000000000, 0.000000000000000000, 1.000000000000000000 ) ) ;
#30844=VECTOR ( 'NONE', #1263, 1000.000000000000000 ) ;
#30846=LINE ( 'NONE', #421, #31837 ) ;
#30863=CARTESIAN_POINT ( 'NONE',  ( 8.000000000000000000, -14.18878633068154826, -6.236773481718229206 ) ) ;
#30877=EDGE_CURVE ( 'NONE', #22597, #20473, #35149, .T. ) ;
#30882=CIRCLE ( 'NONE', #3299, 7.199999999999994849 ) ;
#30910=EDGE_LOOP ( 'NONE', ( #6595, #27368, #26800, #23373 ) ) ;
#30912=ORIENTED_EDGE ( 'NONE', *, *, #4481, .F. ) ;
#30931=DIRECTION ( 'NONE',  ( -1.000000000000000000, 0.000000000000000000, 0.000000000000000000 ) ) ;
#30937=DIRECTION ( 'NONE',  ( 0.000000000000000000, 0.000000000000000000, 1.000000000000000000 ) ) ;
#30942=ORIENTED_EDGE ( 'NONE', *, *, #20458, .T. ) ;
#30952=ORIENTED_EDGE ( 'NONE', *, *, #14115, .T. ) ;
#30961=FACE_OUTER_BOUND ( 'NONE', #7216, .T. ) ;
#30979=DIRECTION ( 'NONE',  ( 0.000000000000000000, 0.8660254037844398178, -0.4999999999999980571 ) ) ;
#30985=DIRECTION ( 'NONE',  ( 0.000000000000000000, 0.000000000000000000, 1.000000000000000000 ) ) ;
#30990=CARTESIAN_POINT ( 'NONE',  ( 0.000000000000000000, 8.605879768205232594, 12.89022243466711437 ) ) ;
#30994=DIRECTION ( 'NONE',  ( 0.000000000000000000, -1.000000000000000000, 0.000000000000000000 ) ) ;
#30998=ORIENTED_EDGE ( 'NONE', *, *, #15910, .F. ) ;
#31092=CIRCLE ( 'NONE', #9830, 7.200000000000006395 ) ;
#31098=ADVANCED_FACE ( 'NONE', ( #30961 ), #17616, .T. ) ;
#31107=DIRECTION ( 'NONE',  ( 0.000000000000000000, 0.9848077530122084644, -0.1736481776669276389 ) ) ;
#31112=AXIS2_PLACEMENT_3D ( 'NONE', #12021, #28064, #34169 ) ;
#31117=CARTESIAN_POINT ( 'NONE',  ( 8.000000000000000000, 0.000000000000000000, 0.000000000000000000 ) ) ;
#31133=ORIENTED_EDGE ( 'NONE', *, *, #35179, .T. ) ;
#31152=CARTESIAN_POINT ( 'NONE',  ( 8.000000000000000000, -16.71027810728550733, 4.579731798933878828 ) ) ;
#31164=DIRECTION ( 'NONE',  ( -1.000000000000000000, 0.000000000000000000, 0.000000000000000000 ) ) ;
#31174=CARTESIAN_POINT ( 'NONE',  ( 8.000000000000000000, 6.071532165918824830E-15, 1.000000000000000000 ) ) ;
#31186=EDGE_LOOP ( 'NONE', ( #24601, #7111, #16987, #22255 ) ) ;
#31200=DIRECTION ( 'NONE',  ( -1.000000000000000000, 0.000000000000000000, 0.000000000000000000 ) ) ;
#31205=DIRECTION ( 'NONE',  ( -1.000000000000000000, 0.000000000000000000, 0.000000000000000000 ) ) ;
#31221=ORIENTED_EDGE ( 'NONE', *, *, #24454, .F. ) ;
#31223=ORIENTED_EDGE ( 'NONE', *, *, #32117, .F. ) ;
#31226=ORIENTED_EDGE ( 'NONE', *, *, #3921, .F. ) ;
#31262=CIRCLE ( 'NONE', #8835, 7.199999999999993960 ) ;
#31265=VERTEX_POINT ( 'NONE', #18154 ) ;
#31273=ORIENTED_EDGE ( 'NONE', *, *, #24871, .T. ) ;
#31278=ORIENTED_EDGE ( 'NONE', *, *, #8852, .T. ) ;
#31282=DIRECTION ( 'NONE',  ( 0.000000000000000000, 0.000000000000000000, 1.000000000000000000 ) ) ;
#31315=CIRCLE ( 'NONE', #16338, 15.49899999999999878 ) ;
#31316=CARTESIAN_POINT ( 'NONE',  ( -10.00000000000000000, 0.000000000000000000, 0.000000000000000000 ) ) ;
#31317=ORIENTED_EDGE ( 'NONE', *, *, #12113, .T. ) ;
#31338=CIRCLE ( 'NONE', #15791, 19.99999999999998579 ) ;
#31342=CARTESIAN_POINT ( 'NONE',  ( 8.000000000000000000, -8.605879768205326741, 12.89022243466705930 ) ) ;
#31352=AXIS2_PLACEMENT_3D ( 'NONE', #25588, #11707, #30979 ) ;
#31355=ORIENTED_EDGE ( 'NONE', *, *, #23562, .T. ) ;
#31357=FACE_OUTER_BOUND ( 'NONE', #23824, .T. ) ;
#31366=CIRCLE ( 'NONE', #7226, 15.49899999999999167 ) ;
#31371=AXIS2_PLACEMENT_3D ( 'NONE', #33884, #17304, #2955 ) ;
#31378=FACE_OUTER_BOUND ( 'NONE', #6677, .T. ) ;
#31391=ORIENTED_EDGE ( 'NONE', *, *, #24415, .F. ) ;
#31396=VERTEX_POINT ( 'NONE', #21388 ) ;
#31403=EDGE_LOOP ( 'NONE', ( #30011, #25957, #5167, #26542 ) ) ;
#31407=CARTESIAN_POINT ( 'NONE',  ( 8.000000000000000000, -17.56975900509168298, -9.555290079479430432 ) ) ;
#31413=VECTOR ( 'NONE', #18931, 1000.000000000000000 ) ;
#31437=ORIENTED_EDGE ( 'NONE', *, *, #15901, .F. ) ;
#31444=ORIENTED_EDGE ( 'NONE', *, *, #6242, .T. ) ;
#31463=ADVANCED_FACE ( 'NONE', ( #21922 ), #8940, .T. ) ;
#31466=DIRECTION ( 'NONE',  ( -1.000000000000000000, 0.000000000000000000, 0.000000000000000000 ) ) ;
#31476=CIRCLE ( 'NONE', #21160, 15.49899999999998279 ) ;
#31480=CARTESIAN_POINT ( 'NONE',  ( 0.000000000000000000, 0.000000000000000000, 0.000000000000000000 ) ) ;
#31487=ORIENTED_EDGE ( 'NONE', *, *, #29564, .F. ) ;
#31507=ADVANCED_FACE ( 'NONE', ( #19727 ), #27700, .T. ) ;
#31509=ORIENTED_EDGE ( 'NONE', *, *, #25810, .F. ) ;
#31517=LINE ( 'NONE', #31152, #30844 ) ;
#31523=ORIENTED_EDGE ( 'NONE', *, *, #2822, .T. ) ;
#31536=ORIENTED_EDGE ( 'NONE', *, *, #8305, .T. ) ;
#31564=CARTESIAN_POINT ( 'NONE',  ( 8.000000000000000000, 16.71027810728552154, 4.579731798933993403 ) ) ;
#31566=ADVANCED_FACE ( 'NONE', ( #3212 ), #25174, .F. ) ;
#31567=ORIENTED_EDGE ( 'NONE', *, *, #14111, .T. ) ;
#31574=VERTEX_POINT ( 'NONE', #19214 ) ;
#31586=CYLINDRICAL_SURFACE ( 'NONE', #6820, 15.49899999999998457 ) ;
#31589=CARTESIAN_POINT ( 'NONE',  ( 0.000000000000000000, -17.56975900509186062, 9.555290079479195953 ) ) ;
#31606=DIRECTION ( 'NONE',  ( 0.000000000000000000, 0.000000000000000000, 1.000000000000000000 ) ) ;
#31612=ORIENTED_EDGE ( 'NONE', *, *, #25743, .T. ) ;
#31631=CARTESIAN_POINT ( 'NONE',  ( 0.000000000000000000, -16.59870953437682672, 3.253005020243791456 ) ) ;
#31656=EDGE_LOOP ( 'NONE', ( #35100, #663, #10318, #7543 ) ) ;
#31688=EDGE_CURVE ( 'NONE', #17618, #26843, #670, .T. ) ;
#31700=AXIS2_PLACEMENT_3D ( 'NONE', #30812, #17292, #11552 ) ;
#31709=VERTEX_POINT ( 'NONE', #23523 ) ;
#31710=CARTESIAN_POINT ( 'NONE',  ( 8.000000000000000000, -5.482169781018935595, 16.00140663693123599 ) ) ;
#31717=VERTEX_POINT ( 'NONE', #23166 ) ;
#31722=DIRECTION ( 'NONE',  ( 0.000000000000000000, -0.9848077530122096857, 0.1736481776669208388 ) ) ;
#31745=EDGE_CURVE ( 'NONE', #1101, #3615, #6959, .T. ) ;
#31747=DIRECTION ( 'NONE',  ( 0.000000000000000000, 0.000000000000000000, 1.000000000000000000 ) ) ;
#31753=CIRCLE ( 'NONE', #22540, 7.199999999999994849 ) ;
#31771=VERTEX_POINT ( 'NONE', #31802 ) ;
#31782=CARTESIAN_POINT ( 'NONE',  ( 8.000000000000000000, -16.71027810728550733, -2.620268201066114688 ) ) ;
#31802=CARTESIAN_POINT ( 'NONE',  ( 0.000000000000000000, -14.87816164169118416, 4.342730381189816136 ) ) ;
#31803=VERTEX_POINT ( 'NONE', #32165 ) ;
#31804=VERTEX_POINT ( 'NONE', #12907 ) ;
#31810=CIRCLE ( 'NONE', #17431, 19.99999999999998579 ) ;
#31811=DIRECTION ( 'NONE',  ( 0.000000000000000000, 0.000000000000000000, -1.000000000000000000 ) ) ;
#31814=CARTESIAN_POINT ( 'NONE',  ( 4.000000000000000000, 17.06000345190455647, -10.43821259704003523 ) ) ;
#31831=CIRCLE ( 'NONE', #18619, 7.200000000000000178 ) ;
#31837=VECTOR ( 'NONE', #596, 1000.000000000000000 ) ;
#31846=CIRCLE ( 'NONE', #7124, 7.199999999999994849 ) ;
#31883=ORIENTED_EDGE ( 'NONE', *, *, #19209, .T. ) ;
#31919=EDGE_CURVE ( 'NONE', #4062, #10084, #21385, .T. ) ;
#31926=ORIENTED_EDGE ( 'NONE', *, *, #31745, .T. ) ;
#31930=CARTESIAN_POINT ( 'NONE',  ( 0.000000000000000000, -3.678165988948486564, -15.05623113391070866 ) ) ;
#31952=CARTESIAN_POINT ( 'NONE',  ( 0.000000000000000000, 0.000000000000000000, 0.000000000000000000 ) ) ;
#31973=LINE ( 'NONE', #21164, #4768 ) ;
#32002=CARTESIAN_POINT ( 'NONE',  ( 0.000000000000000000, -14.18878633068162998, 6.236773481718038248 ) ) ;
#32017=ORIENTED_EDGE ( 'NONE', *, *, #26389, .F. ) ;
#32019=EDGE_CURVE ( 'NONE', #5508, #26760, #1273, .T. ) ;
#32026=VECTOR ( 'NONE', #5151, 1000.000000000000000 ) ;
#32027=DIRECTION ( 'NONE',  ( -1.000000000000000000, 0.000000000000000000, 0.000000000000000000 ) ) ;
#32061=ORIENTED_EDGE ( 'NONE', *, *, #35267, .F. ) ;
#32069=AXIS2_PLACEMENT_3D ( 'NONE', #9163, #23204, #22841 ) ;
#32073=ORIENTED_EDGE ( 'NONE', *, *, #15628, .T. ) ;
#32076=EDGE_CURVE ( 'NONE', #23216, #18735, #31753, .T. ) ;
#32085=ORIENTED_EDGE ( 'NONE', *, *, #6011, .T. ) ;
#32097=VERTEX_POINT ( 'NONE', #5862 ) ;
#32098=DIRECTION ( 'NONE',  ( 0.000000000000000000, 0.000000000000000000, 1.000000000000000000 ) ) ;
#32100=DIRECTION ( 'NONE',  ( -1.000000000000000000, 0.000000000000000000, 0.000000000000000000 ) ) ;
#32109=ORIENTED_EDGE ( 'NONE', *, *, #11042, .T. ) ;
#32117=EDGE_CURVE ( 'NONE', #11984, #17379, #26579, .T. ) ;
#32141=LINE ( 'NONE', #18450, #32026 ) ;
#32155=ORIENTED_EDGE ( 'NONE', *, *, #12113, .F. ) ;
#32161=ORIENTED_EDGE ( 'NONE', *, *, #11760, .F. ) ;
#32165=CARTESIAN_POINT ( 'NONE',  ( 0.000000000000000000, -7.317194182740271557, 18.61340026142649506 ) ) ;
#32166=ORIENTED_EDGE ( 'NONE', *, *, #27794, .T. ) ;
#32176=DIRECTION ( 'NONE',  ( 0.000000000000000000, -0.9848077530122062440, -0.1736481776669404065 ) ) ;
#32194=DIRECTION ( 'NONE',  ( 1.000000000000000000, -0.000000000000000000, 0.000000000000000000 ) ) ;
#32204=ADVANCED_FACE ( 'NONE', ( #3700 ), #1172, .T. ) ;
#32209=ORIENTED_EDGE ( 'NONE', *, *, #21404, .T. ) ;
#32220=EDGE_CURVE ( 'NONE', #18539, #5366, #25663, .T. ) ;
#32241=VERTEX_POINT ( 'NONE', #31407 ) ;
#32242=PLANE ( 'NONE',  #15719 ) ;
#32246=CIRCLE ( 'NONE', #9234, 15.49899999999998634 ) ;
#32257=DIRECTION ( 'NONE',  ( 1.000000000000000000, -0.000000000000000000, -0.000000000000000000 ) ) ;
#32258=ORIENTED_EDGE ( 'NONE', *, *, #25078, .T. ) ;
#32273=VERTEX_POINT ( 'NONE', #2263 ) ;
#32306=DIRECTION ( 'NONE',  ( -1.000000000000000000, 0.000000000000000000, 0.000000000000000000 ) ) ;
#32312=DIRECTION ( 'NONE',  ( -1.000000000000000000, 0.000000000000000000, 0.000000000000000000 ) ) ;
#32326=FACE_OUTER_BOUND ( 'NONE', #6210, .T. ) ;
#32327=CARTESIAN_POINT ( 'NONE',  ( 0.000000000000000000, -16.59870953437678409, -3.253005020244019718 ) ) ;
#32337=CYLINDRICAL_SURFACE ( 'NONE', #2252, 7.199999999999994849 ) ;
#32357=DIRECTION ( 'NONE',  ( 0.000000000000000000, 0.9848077530122073542, 0.1736481776669339394 ) ) ;
#32374=CIRCLE ( 'NONE', #16830, 15.49899999999998812 ) ;
#32418=ORIENTED_EDGE ( 'NONE', *, *, #19805, .F. ) ;
#32431=ORIENTED_EDGE ( 'NONE', *, *, #20212, .F. ) ;
#32445=VECTOR ( 'NONE', #5376, 1000.000000000000000 ) ;
#32449=DIRECTION ( 'NONE',  ( -1.000000000000000000, 0.000000000000000000, 0.000000000000000000 ) ) ;
#32450=CYLINDRICAL_SURFACE ( 'NONE', #23759, 7.199999999999993960 ) ;
#32467=ORIENTED_EDGE ( 'NONE', *, *, #2296, .T. ) ;
#32478=ORIENTED_EDGE ( 'NONE', *, *, #241, .T. ) ;
#32483=DIRECTION ( 'NONE',  ( 0.000000000000000000, 0.000000000000000000, 1.000000000000000000 ) ) ;
#32498=DIRECTION ( 'NONE',  ( -1.000000000000000000, 0.000000000000000000, 0.000000000000000000 ) ) ;
#32500=CARTESIAN_POINT ( 'NONE',  ( 4.000000000000000000, 19.60123832284022782, -3.973846525876241653 ) ) ;
#32536=ORIENTED_EDGE ( 'NONE', *, *, #1246, .F. ) ;
#32544=ORIENTED_EDGE ( 'NONE', *, *, #30556, .F. ) ;
#32547=VECTOR ( 'NONE', #9822, 1000.000000000000000 ) ;
#32554=AXIS2_PLACEMENT_3D ( 'NONE', #3540, #25867, #14317 ) ;
#32558=DIRECTION ( 'NONE',  ( 0.000000000000000000, 0.000000000000000000, 1.000000000000000000 ) ) ;
#32571=EDGE_CURVE ( 'NONE', #12650, #5366, #12229, .T. ) ;
#32584=DIRECTION ( 'NONE',  ( -1.000000000000000000, 0.000000000000000000, 0.000000000000000000 ) ) ;
#32588=ADVANCED_FACE ( 'NONE', ( #10694 ), #22018, .T. ) ;
#32590=DIRECTION ( 'NONE',  ( 1.000000000000000000, -0.000000000000000000, 0.000000000000000000 ) ) ;
#32593=VERTEX_POINT ( 'NONE', #18967 ) ;
#32606=ORIENTED_EDGE ( 'NONE', *, *, #24381, .T. ) ;
#32610=AXIS2_PLACEMENT_3D ( 'NONE', #2326, #10943, #35091 ) ;
#32611=CIRCLE ( 'NONE', #398, 7.199999999999993072 ) ;
#32617=DIRECTION ( 'NONE',  ( -1.000000000000000000, 0.000000000000000000, 0.000000000000000000 ) ) ;
#32638=DIRECTION ( 'NONE',  ( -1.000000000000000000, 0.000000000000000000, 0.000000000000000000 ) ) ;
#32647=VERTEX_POINT ( 'NONE', #20313 ) ;
#32654=ORIENTED_EDGE ( 'NONE', *, *, #23357, .F. ) ;
#32691=AXIS2_PLACEMENT_3D ( 'NONE', #943, #11400, #33009 ) ;
#32697=VERTEX_POINT ( 'NONE', #26105 ) ;
#32703=VERTEX_POINT ( 'NONE', #18162 ) ;
#32758=DIRECTION ( 'NONE',  ( -1.000000000000000000, 0.000000000000000000, 0.000000000000000000 ) ) ;
#32759=ORIENTED_EDGE ( 'NONE', *, *, #25639, .F. ) ;
#32770=CARTESIAN_POINT ( 'NONE',  ( 0.000000000000000000, 6.860320204751148232, 13.89802171851385459 ) ) ;
#32778=DIRECTION ( 'NONE',  ( -1.000000000000000000, 0.000000000000000000, 0.000000000000000000 ) ) ;
#32784=ORIENTED_EDGE ( 'NONE', *, *, #14324, .T. ) ;
#32788=AXIS2_PLACEMENT_3D ( 'NONE', #7474, #20606, #31606 ) ;
#32806=CYLINDRICAL_SURFACE ( 'NONE', #20659, 19.99999999999998579 ) ;
#32815=CYLINDRICAL_SURFACE ( 'NONE', #3521, 7.199999999999993072 ) ;
#32818=AXIS2_PLACEMENT_3D ( 'NONE', #35325, #10645, #16021 ) ;
#32822=DIRECTION ( 'NONE',  ( 1.000000000000000000, -0.000000000000000000, -0.000000000000000000 ) ) ;
#32835=DIRECTION ( 'NONE',  ( -1.000000000000000000, 0.000000000000000000, 0.000000000000000000 ) ) ;
#32837=CARTESIAN_POINT ( 'NONE',  ( 8.000000000000000000, 1.693188892523745936, 15.40623615209872632 ) ) ;
#32859=DIRECTION ( 'NONE',  ( -1.000000000000000000, 0.000000000000000000, 0.000000000000000000 ) ) ;
#32860=CIRCLE ( 'NONE', #27111, 7.199999999999993072 ) ;
#32867=CARTESIAN_POINT ( 'NONE',  ( -10.00000000000000000, 0.000000000000000000, 0.000000000000000000 ) ) ;
#32874=ORIENTED_EDGE ( 'NONE', *, *, #16477, .F. ) ;
#32875=ORIENTED_EDGE ( 'NONE', *, *, #3046, .F. ) ;
#32876=DIRECTION ( 'NONE',  ( 0.000000000000000000, -0.3420201433256566115, -0.9396926207859127578 ) ) ;
#32879=DIRECTION ( 'NONE',  ( 0.000000000000000000, -0.3420201433256566115, -0.9396926207859127578 ) ) ;
#32885=ADVANCED_FACE ( 'NONE', ( #21562 ), #24295, .F. ) ;
#32887=LINE ( 'NONE', #30369, #30085 ) ;
#32892=VECTOR ( 'NONE', #3526, 1000.000000000000000 ) ;
#32898=FACE_OUTER_BOUND ( 'NONE', #31656, .T. ) ;
#32915=DIRECTION ( 'NONE',  ( 0.000000000000000000, 0.000000000000000000, 1.000000000000000000 ) ) ;
#33009=DIRECTION ( 'NONE',  ( 0.000000000000000000, 0.000000000000000000, 1.000000000000000000 ) ) ;
#33013=DIRECTION ( 'NONE',  ( -1.000000000000000000, 0.000000000000000000, 0.000000000000000000 ) ) ;
#33015=AXIS2_PLACEMENT_3D ( 'NONE', #30434, #695, #14207 ) ;
#33023=DIRECTION ( 'NONE',  ( 0.000000000000000000, 0.000000000000000000, 1.000000000000000000 ) ) ;
#33043=AXIS2_PLACEMENT_3D ( 'NONE', #34715, #1950, #21366 ) ;
#33045=DIRECTION ( 'NONE',  ( 0.000000000000000000, 0.000000000000000000, 1.000000000000000000 ) ) ;
#33055=CYLINDRICAL_SURFACE ( 'NONE', #30397, 7.199999999999993960 ) ;
#33059=DIRECTION ( 'NONE',  ( 0.000000000000000000, 0.3420201433256692680, -0.9396926207859080948 ) ) ;
#33061=CARTESIAN_POINT ( 'NONE',  ( 8.000000000000000000, -8.605879768205133118, -12.89022243466717299 ) ) ;
#33084=AXIS2_PLACEMENT_3D ( 'NONE', #28858, #17319, #20367 ) ;
#33087=CARTESIAN_POINT ( 'NONE',  ( 0.000000000000000000, -16.59870953437682672, 10.45300502024378986 ) ) ;
#33104=AXIS2_PLACEMENT_3D ( 'NONE', #15108, #3628, #9550 ) ;
#33111=ORIENTED_EDGE ( 'NONE', *, *, #15178, .F. ) ;
#33121=ORIENTED_EDGE ( 'NONE', *, *, #31745, .F. ) ;
#33132=DIRECTION ( 'NONE',  ( 1.000000000000000000, -0.000000000000000000, -0.000000000000000000 ) ) ;
#33134=ORIENTED_EDGE ( 'NONE', *, *, #7291, .T. ) ;
#33143=DIRECTION ( 'NONE',  ( -1.000000000000000000, 0.000000000000000000, 0.000000000000000000 ) ) ;
#33158=EDGE_CURVE ( 'NONE', #28443, #15919, #2891, .T. ) ;
#33164=ORIENTED_EDGE ( 'NONE', *, *, #17483, .F. ) ;
#33179=ORIENTED_EDGE ( 'NONE', *, *, #35297, .F. ) ;
#33180=AXIS2_PLACEMENT_3D ( 'NONE', #7870, #32194, #18859 ) ;
#33184=ORIENTED_EDGE ( 'NONE', *, *, #32220, .F. ) ;
#33185=ORIENTED_EDGE ( 'NONE', *, *, #34804, .F. ) ;
#33208=CARTESIAN_POINT ( 'NONE',  ( 0.000000000000000000, 5.482169781018835231, 16.00140663693125376 ) ) ;
#33216=CYLINDRICAL_SURFACE ( 'NONE', #17601, 19.99999999999998579 ) ;
#33232=DIRECTION ( 'NONE',  ( -1.000000000000000000, 0.000000000000000000, 0.000000000000000000 ) ) ;
#33247=CARTESIAN_POINT ( 'NONE',  ( 0.000000000000000000, 11.11653975335807587, -12.74840161668719851 ) ) ;
#33249=DIRECTION ( 'NONE',  ( 0.000000000000000000, 0.000000000000000000, -1.000000000000000000 ) ) ;
#33250=DIRECTION ( 'NONE',  ( 0.000000000000000000, 0.000000000000000000, -1.000000000000000000 ) ) ;
#33258=CARTESIAN_POINT ( 'NONE',  ( 0.000000000000000000, -14.48509162075955281, -8.733917826871511636 ) ) ;
#33267=DIRECTION ( 'NONE',  ( 0.000000000000000000, 0.000000000000000000, 1.000000000000000000 ) ) ;
#33268=CIRCLE ( 'NONE', #5676, 15.49899999999998457 ) ;
#33272=ORIENTED_EDGE ( 'NONE', *, *, #13714, .T. ) ;
#33304=CARTESIAN_POINT ( 'NONE',  ( 0.000000000000000000, 5.400000000000000355, 0.000000000000000000 ) ) ;
#33313=VERTEX_POINT ( 'NONE', #13951 ) ;
#33351=ORIENTED_EDGE ( 'NONE', *, *, #10929, .F. ) ;
#33368=CARTESIAN_POINT ( 'NONE',  ( 8.000000000000000000, 13.24207120356965461, 14.98824707027445768 ) ) ;
#33371=VERTEX_POINT ( 'NONE', #33560 ) ;
#33376=ORIENTED_EDGE ( 'NONE', *, *, #29564, .T. ) ;
#33377=DIRECTION ( 'NONE',  ( -1.000000000000000000, 0.000000000000000000, 0.000000000000000000 ) ) ;
#33388=CIRCLE ( 'NONE', #5245, 19.99999999999998579 ) ;
#33390=EDGE_LOOP ( 'NONE', ( #16894, #28283, #11001, #7138 ) ) ;
#33412=CYLINDRICAL_SURFACE ( 'NONE', #32554, 7.199999999999993072 ) ;
#33426=CYLINDRICAL_SURFACE ( 'NONE', #28663, 15.49899999999998457 ) ;
#33433=DIRECTION ( 'NONE',  ( 0.000000000000000000, 0.000000000000000000, 1.000000000000000000 ) ) ;
#33440=EDGE_CURVE ( 'NONE', #34283, #2896, #28606, .T. ) ;
#33448=DIRECTION ( 'NONE',  ( -1.000000000000000000, 0.000000000000000000, 0.000000000000000000 ) ) ;
#33468=CARTESIAN_POINT ( 'NONE',  ( 8.000000000000000000, -16.59870953437682672, 10.45300502024378453 ) ) ;
#33477=VERTEX_POINT ( 'NONE', #32770 ) ;
#33490=AXIS2_PLACEMENT_3D ( 'NONE', #6883, #32617, #19099 ) ;
#33499=ORIENTED_EDGE ( 'NONE', *, *, #18723, .F. ) ;
#33506=CARTESIAN_POINT ( 'NONE',  ( 4.000000000000000000, -17.56975900509186062, 9.555290079479195953 ) ) ;
#33515=ORIENTED_EDGE ( 'NONE', *, *, #30824, .T. ) ;
#33543=VECTOR ( 'NONE', #28237, 1000.000000000000000 ) ;
#33547=DIRECTION ( 'NONE',  ( -1.000000000000000000, 0.000000000000000000, 0.000000000000000000 ) ) ;
#33552=ADVANCED_FACE ( 'NONE', ( #13691 ), #24671, .T. ) ;
#33560=CARTESIAN_POINT ( 'NONE',  ( 0.000000000000000000, 17.06000345190438949, 10.43821259704026794 ) ) ;
#33561=DIRECTION ( 'NONE',  ( -1.000000000000000000, 0.000000000000000000, 0.000000000000000000 ) ) ;
#33586=EDGE_CURVE ( 'NONE', #10915, #21999, #12543, .T. ) ;
#33629=EDGE_CURVE ( 'NONE', #10783, #932, #25740, .T. ) ;
#33641=CARTESIAN_POINT ( 'NONE',  ( 8.000000000000000000, -6.359167119270591861, 18.96209359615091827 ) ) ;
#33674=EDGE_CURVE ( 'NONE', #26725, #2211, #6456, .T. ) ;
#33679=FACE_OUTER_BOUND ( 'NONE', #34050, .T. ) ;
#33680=AXIS2_PLACEMENT_3D ( 'NONE', #28950, #10038, #18665 ) ;
#33691=ORIENTED_EDGE ( 'NONE', *, *, #637, .F. ) ;
#33696=ORIENTED_EDGE ( 'NONE', *, *, #3812, .F. ) ;
#33707=VERTEX_POINT ( 'NONE', #33641 ) ;
#33726=EDGE_CURVE ( 'NONE', #11394, #9366, #22836, .T. ) ;
#33734=DIRECTION ( 'NONE',  ( 0.000000000000000000, 0.3420201433256695456, -0.9396926207859079838 ) ) ;
#33738=FACE_OUTER_BOUND ( 'NONE', #10833, .T. ) ;
#33741=EDGE_LOOP ( 'NONE', ( #5077, #4165, #2534, #31509 ) ) ;
#33757=CIRCLE ( 'NONE', #21666, 15.49899999999998101 ) ;
#33778=AXIS2_PLACEMENT_3D ( 'NONE', #35421, #29847, #27504 ) ;
#33825=DIRECTION ( 'NONE',  ( -1.000000000000000000, 0.000000000000000000, 0.000000000000000000 ) ) ;
#33852=DIRECTION ( 'NONE',  ( -1.000000000000000000, 0.000000000000000000, 0.000000000000000000 ) ) ;
#33857=DIRECTION ( 'NONE',  ( 0.000000000000000000, 0.000000000000000000, 1.000000000000000000 ) ) ;
#33862=AXIS2_PLACEMENT_3D ( 'NONE', #22939, #33232, #33938 ) ;
#33874=CARTESIAN_POINT ( 'NONE',  ( 8.000000000000000000, -0.5097555531871945655, -19.99350267651956159 ) ) ;
#33884=CARTESIAN_POINT ( 'NONE',  ( 8.000000000000000000, 0.000000000000000000, 0.000000000000000000 ) ) ;
#33906=FACE_OUTER_BOUND ( 'NONE', #28865, .T. ) ;
#33910=CIRCLE ( 'NONE', #17781, 7.199999999999995737 ) ;
#33938=DIRECTION ( 'NONE',  ( 0.000000000000000000, 0.000000000000000000, 1.000000000000000000 ) ) ;
#33954=DIRECTION ( 'NONE',  ( 0.000000000000000000, 0.000000000000000000, 1.000000000000000000 ) ) ;
#33966=EDGE_CURVE ( 'NONE', #27370, #10671, #13645, .T. ) ;
#33976=EDGE_LOOP ( 'NONE', ( #14430, #11132, #10021, #449 ) ) ;
#34007=DIRECTION ( 'NONE',  ( -1.000000000000000000, 0.000000000000000000, 0.000000000000000000 ) ) ;
#34012=EDGE_CURVE ( 'NONE', #18147, #26998, #32611, .T. ) ;
#34048=ORIENTED_EDGE ( 'NONE', *, *, #1246, .T. ) ;
#34050=EDGE_LOOP ( 'NONE', ( #15844, #18782, #35494, #35127 ) ) ;
#34055=DIRECTION ( 'NONE',  ( 1.000000000000000000, -0.000000000000000000, 0.000000000000000000 ) ) ;
#34067=ORIENTED_EDGE ( 'NONE', *, *, #16324, .F. ) ;
#34072=ORIENTED_EDGE ( 'NONE', *, *, #5554, .F. ) ;
#34089=CARTESIAN_POINT ( 'NONE',  ( 4.000000000000000000, 17.06000345190438949, 10.43821259704026794 ) ) ;
#34107=ADVANCED_FACE ( 'NONE', ( #20077 ), #33426, .T. ) ;
#34114=VECTOR ( 'NONE', #17326, 1000.000000000000000 ) ;
#34120=VECTOR ( 'NONE', #7442, 1000.000000000000000 ) ;
#34132=VECTOR ( 'NONE', #20456, 1000.000000000000000 ) ;
#34150=ORIENTED_EDGE ( 'NONE', *, *, #3532, .T. ) ;
#34164=CARTESIAN_POINT ( 'NONE',  ( 0.000000000000000000, 17.56975900509174693, 9.555290079479316745 ) ) ;
#34169=DIRECTION ( 'NONE',  ( 0.000000000000000000, 0.8660254037844363761, 0.5000000000000037748 ) ) ;
#34196=VECTOR ( 'NONE', #21193, 1000.000000000000000 ) ;
#34225=LINE ( 'NONE', #26490, #16853 ) ;
#34283=VERTEX_POINT ( 'NONE', #12538 ) ;
#34287=MANIFOLD_SOLID_BREP ( 'Keyway', #18681 ) ;
#34294=AXIS2_PLACEMENT_3D ( 'NONE', #14756, #14570, #33857 ) ;
#34330=EDGE_LOOP ( 'NONE', ( #23476, #10586, #14724, #9448 ) ) ;
#34352=AXIS2_PLACEMENT_3D ( 'NONE', #10927, #35417, #35243 ) ;
#34355=ADVANCED_FACE ( 'NONE', ( #18639 ), #4975, .T. ) ;
#34362=VECTOR ( 'NONE', #30086, 1000.000000000000000 ) ;
#34364=CARTESIAN_POINT ( 'NONE',  ( 0.000000000000000000, 16.59870953437680896, 10.45300502024390354 ) ) ;
#34377=ORIENTED_EDGE ( 'NONE', *, *, #5122, .T. ) ;
#34383=PRODUCT_DEFINITION ( 'UNKNOWN', '', #29921, #408 ) ;
#34395=ADVANCED_FACE ( 'NONE', ( #32326 ), #21501, .T. ) ;
#34397=ORIENTED_EDGE ( 'NONE', *, *, #30229, .T. ) ;
#34398=AXIS2_PLACEMENT_3D ( 'NONE', #5762, #23651, #20919 ) ;
#34405=DIRECTION ( 'NONE',  ( -1.000000000000000000, 0.000000000000000000, 0.000000000000000000 ) ) ;
#34441=AXIS2_PLACEMENT_3D ( 'NONE', #20797, #15754, #23518 ) ;
#34457=CYLINDRICAL_SURFACE ( 'NONE', #9929, 3.999999999999996447 ) ;
#34461=CARTESIAN_POINT ( 'NONE',  ( 50.00005079999999680, 3.872983346207417021, 0.9999999999999985567 ) ) ;
#34463=CARTESIAN_POINT ( 'NONE',  ( 8.000000000000000000, 0.000000000000000000, 0.000000000000000000 ) ) ;
#34485=DIRECTION ( 'NONE',  ( 0.000000000000000000, 0.6427876096865403621, -0.7660444431189772363 ) ) ;
#34502=CARTESIAN_POINT ( 'NONE',  ( 8.000000000000000000, 8.605879768205412006, -12.89022243466699535 ) ) ;
#34524=VERTEX_POINT ( 'NONE', #14291 ) ;
#34557=CARTESIAN_POINT ( 'NONE',  ( -10.00000000000000000, 0.000000000000000000, 0.000000000000000000 ) ) ;
#34568=AXIS2_PLACEMENT_3D ( 'NONE', #16222, #32638, #24889 ) ;
#34582=FACE_OUTER_BOUND ( 'NONE', #20139, .T. ) ;
#34649=AXIS2_PLACEMENT_3D ( 'NONE', #25483, #28353, #28890 ) ;
#34651=ORIENTED_EDGE ( 'NONE', *, *, #16752, .T. ) ;
#34662=EDGE_CURVE ( 'NONE', #10377, #14262, #23348, .T. ) ;
#34663=CIRCLE ( 'NONE', #26052, 15.49899999999998279 ) ;
#34664=AXIS2_PLACEMENT_3D ( 'NONE', #1986, #13495, #10267 ) ;
#34671=CARTESIAN_POINT ( 'NONE',  ( 4.000000000000000000, 19.77827456857338007, 2.969824084036535528 ) ) ;
#34695=CIRCLE ( 'NONE', #34664, 19.99999999999998579 ) ;
#34696=LINE ( 'NONE', #2425, #18307 ) ;
#34698=ORIENTED_EDGE ( 'NONE', *, *, #26628, .F. ) ;
#34699=ORIENTED_EDGE ( 'NONE', *, *, #3170, .T. ) ;
#34715=CARTESIAN_POINT ( 'NONE',  ( 8.000000000000000000, 0.000000000000000000, 0.000000000000000000 ) ) ;
#34747=ADVANCED_FACE ( 'NONE', ( #6727 ), #14829, .T. ) ;
#34768=CIRCLE ( 'NONE', #10052, 15.49899999999998279 ) ;
#34784=ORIENTED_EDGE ( 'NONE', *, *, #15910, .T. ) ;
#34793=CIRCLE ( 'NONE', #15197, 7.199999999999993960 ) ;
#34801=AXIS2_PLACEMENT_3D ( 'NONE', #8235, #19212, #27861 ) ;
#34804=EDGE_CURVE ( 'NONE', #6961, #11554, #13383, .T. ) ;
#34828=VERTEX_POINT ( 'NONE', #35183 ) ;
#34837=DIRECTION ( 'NONE',  ( -1.000000000000000000, 0.000000000000000000, 0.000000000000000000 ) ) ;
#34852=DIRECTION ( 'NONE',  ( 1.000000000000000000, -0.000000000000000000, 0.000000000000000000 ) ) ;
#34857=AXIS2_PLACEMENT_3D ( 'NONE', #6277, #19936, #28607 ) ;
#34869=DIRECTION ( 'NONE',  ( 0.000000000000000000, 0.000000000000000000, 1.000000000000000000 ) ) ;
#34882=DIRECTION ( 'NONE',  ( 0.000000000000000000, 0.000000000000000000, -1.000000000000000000 ) ) ;
#34885=VECTOR ( 'NONE', #16456, 1000.000000000000000 ) ;
#34893=VECTOR ( 'NONE', #35424, 1000.000000000000000 ) ;
#34910=CARTESIAN_POINT ( 'NONE',  ( 8.000000000000000000, 0.000000000000000000, 0.000000000000000000 ) ) ;
#34911=CIRCLE ( 'NONE', #2710, 7.199999999999991296 ) ;
#34928=VECTOR ( 'NONE', #6798, 1000.000000000000000 ) ;
#34967=CIRCLE ( 'NONE', #3916, 7.199999999999994849 ) ;
#34986=DIRECTION ( 'NONE',  ( 0.000000000000000000, 0.000000000000000000, 1.000000000000000000 ) ) ;
#34998=CARTESIAN_POINT ( 'NONE',  ( 0.000000000000000000, 14.18878633068160866, 6.236773481718133283 ) ) ;
#35014=AXIS2_PLACEMENT_3D ( 'NONE', #15940, #35234, #32876 ) ;
#35032=CYLINDRICAL_SURFACE ( 'NONE', #24350, 19.99999999999998579 ) ;
#35058=ADVANCED_FACE ( 'NONE', ( #25430 ), #393, .T. ) ;
#35080=DIRECTION ( 'NONE',  ( -1.000000000000000000, 0.000000000000000000, 0.000000000000000000 ) ) ;
#35081=ADVANCED_FACE ( 'NONE', ( #1284 ), #26134, .T. ) ;
#35086=DIRECTION ( 'NONE',  ( 0.000000000000000000, 0.000000000000000000, 1.000000000000000000 ) ) ;
#35091=DIRECTION ( 'NONE',  ( 0.000000000000000000, 0.9848077530122084644, -0.1736481776669276389 ) ) ;
#35095=CARTESIAN_POINT ( 'NONE',  ( 8.000000000000000000, -14.48509162075955281, -8.733917826871511636 ) ) ;
#35097=ORIENTED_EDGE ( 'NONE', *, *, #15664, .T. ) ;
#35100=ORIENTED_EDGE ( 'NONE', *, *, #2926, .T. ) ;
#35125=FACE_OUTER_BOUND ( 'NONE', #5732, .T. ) ;
#35127=ORIENTED_EDGE ( 'NONE', *, *, #23354, .T. ) ;
#35143=CARTESIAN_POINT ( 'NONE',  ( 8.000000000000000000, -15.46619997295643856, 1.007799283846635863 ) ) ;
#35149=CIRCLE ( 'NONE', #32818, 7.199999999999994849 ) ;
#35151=CARTESIAN_POINT ( 'NONE',  ( 8.000000000000000000, 0.000000000000000000, 0.000000000000000000 ) ) ;
#35164=DIRECTION ( 'NONE',  ( 0.000000000000000000, -0.3420201433256755963, 0.9396926207859057634 ) ) ;
#35170=DIRECTION ( 'NONE',  ( -1.000000000000000000, 0.000000000000000000, 0.000000000000000000 ) ) ;
#35179=EDGE_CURVE ( 'NONE', #6533, #4002, #20168, .T. ) ;
#35183=CARTESIAN_POINT ( 'NONE',  ( 8.000000000000000000, 4.898587196589413815E-16, -4.000000000000000000 ) ) ;
#35202=AXIS2_PLACEMENT_3D ( 'NONE', #21575, #10448, #29707 ) ;
#35205=CARTESIAN_POINT ( 'NONE',  ( 8.000000000000000000, -19.77827456857337651, 2.969824084036393863 ) ) ;
#35214=CARTESIAN_POINT ( 'NONE',  ( 8.000000000000000000, 0.000000000000000000, 0.000000000000000000 ) ) ;
#35221=DIRECTION ( 'NONE',  ( -1.000000000000000000, 0.000000000000000000, 0.000000000000000000 ) ) ;
#35224=EDGE_LOOP ( 'NONE', ( #17309, #8791, #12072, #26492 ) ) ;
#35234=DIRECTION ( 'NONE',  ( -1.000000000000000000, 0.000000000000000000, 0.000000000000000000 ) ) ;
#35243=DIRECTION ( 'NONE',  ( 0.000000000000000000, 0.000000000000000000, -1.000000000000000000 ) ) ;
#35246=EDGE_CURVE ( 'NONE', #4579, #6999, #29207, .T. ) ;
#35267=EDGE_CURVE ( 'NONE', #10084, #5612, #29906, .T. ) ;
#35275=CYLINDRICAL_SURFACE ( 'NONE', #1027, 7.199999999999993960 ) ;
#35285=DIRECTION ( 'NONE',  ( -1.000000000000000000, 0.000000000000000000, 0.000000000000000000 ) ) ;
#35286=EDGE_CURVE ( 'NONE', #34828, #27661, #27211, .T. ) ;
#35297=EDGE_CURVE ( 'NONE', #13349, #1026, #6721, .T. ) ;
#35322=ORIENTED_EDGE ( 'NONE', *, *, #29917, .F. ) ;
#35325=CARTESIAN_POINT ( 'NONE',  ( 0.000000000000000000, -11.11653975335780942, -12.74840161668743299 ) ) ;
#35334=CYLINDRICAL_SURFACE ( 'NONE', #1075, 7.199999999999993960 ) ;
#35349=CARTESIAN_POINT ( 'NONE',  ( 0.000000000000000000, -0.3212489022566501484, 16.91141623315869680 ) ) ;
#35358=SHAPE_REPRESENTATION_RELATIONSHIP ( 'NONE' , 'NONE' ,  #11863, #1766 ) ;
#35382=CARTESIAN_POINT ( 'NONE',  ( 8.000000000000000000, 0.000000000000000000, 0.000000000000000000 ) ) ;
#35388=CARTESIAN_POINT ( 'NONE',  ( 8.000000000000000000, 0.000000000000000000, 0.000000000000000000 ) ) ;
#35398=CYLINDRICAL_SURFACE ( 'NONE', #11100, 7.199999999999994849 ) ;
#35404=ORIENTED_EDGE ( 'NONE', *, *, #4363, .T. ) ;
#35408=DIRECTION ( 'NONE',  ( 1.000000000000000000, -0.000000000000000000, 0.000000000000000000 ) ) ;
#35409=ORIENTED_EDGE ( 'NONE', *, *, #16384, .T. ) ;
#35414=EDGE_CURVE ( 'NONE', #26625, #34828, #1178, .T. ) ;
#35417=DIRECTION ( 'NONE',  ( -1.000000000000000000, 0.000000000000000000, -0.000000000000000000 ) ) ;
#35421=CARTESIAN_POINT ( 'NONE',  ( 8.000000000000000000, 16.71027810728552154, -2.620268201066000113 ) ) ;
#35424=DIRECTION ( 'NONE',  ( -1.000000000000000000, 0.000000000000000000, 0.000000000000000000 ) ) ;
#35443=AXIS2_PLACEMENT_3D ( 'NONE', #7828, #35221, #10538 ) ;
#35444=EDGE_CURVE ( 'NONE', #11499, #17618, #28780, .T. ) ;
#35447=DIRECTION ( 'NONE',  ( -1.000000000000000000, 0.000000000000000000, 0.000000000000000000 ) ) ;
#35448=ADVANCED_FACE ( 'NONE', ( #24501 ), #30775, .T. ) ;
#35449=AXIS2_PLACEMENT_3D ( 'NONE', #1327, #1157, #31747 ) ;
#35455=EDGE_CURVE ( 'NONE', #28345, #1645, #2918, .T. ) ;
#35456=CARTESIAN_POINT ( 'NONE',  ( 50.00005079999999680, 0.000000000000000000, 0.000000000000000000 ) ) ;
#35457=EDGE_LOOP ( 'NONE', ( #26956, #15164, #21701, #1638 ) ) ;
#35459=EDGE_CURVE ( 'NONE', #7443, #1605, #30505, .T. ) ;
#35479=CARTESIAN_POINT ( 'NONE',  ( 8.000000000000000000, -16.59870953437682672, 10.45300502024378986 ) ) ;
#35494=ORIENTED_EDGE ( 'NONE', *, *, #13687, .T. ) ;
#35500=ORIENTED_EDGE ( 'NONE', *, *, #3812, .T. ) ;
#35511=DIRECTION ( 'NONE',  ( 0.000000000000000000, 0.000000000000000000, 1.000000000000000000 ) ) ;
#35545=AXIS2_PLACEMENT_3D ( 'NONE', #20192, #31200, #32098 ) ;
#35546=DIRECTION ( 'NONE',  ( 0.000000000000000000, -0.6427876096865456912, 0.7660444431189726844 ) ) ;
#35552=CIRCLE ( 'NONE', #21152, 15.49899999999998279 ) ;
#35582=EDGE_LOOP ( 'NONE', ( #25291, #31226, #19992, #13934 ) ) ;
#35613=CARTESIAN_POINT ( 'NONE',  ( 8.000000000000000000, 11.19999565274265230, -10.71350075272062874 ) ) ;
#35614=CARTESIAN_POINT ( 'NONE',  ( 8.000000000000000000, -3.678165988948685516, 15.05623113391066070 ) ) ;
ENDSEC;
END-ISO-10303-21;
